ISO-10303-21;
HEADER;
FILE_DESCRIPTION (('STEP AP214'),
    '1' );
FILE_NAME ('Support Ledge.step',
    '2026-10-26T17:37:43',
    ( '' ),
    ( '' ),
    'SwSTEP 2.0',
    'SolidWorks 2024',
    '' );
FILE_SCHEMA (( 'AUTOMOTIVE_DESIGN' ));
ENDSEC;

DATA;
#17=ORIENTED_EDGE ( 'NONE', *, *, #15739, .F. ) ;
#42=EDGE_LOOP ( 'NONE', ( #2703, #1001, #9067, #21720 ) ) ;
#56=EDGE_LOOP ( 'NONE', ( #1910, #7184, #18432, #2575 ) ) ;
#74=DIRECTION ( 'NONE',  ( 0.000000000000000000, 0.000000000000000000, 1.000000000000000000 ) ) ;
#94=CARTESIAN_POINT ( 'NONE',  ( 3.048000000000000043, -3544.061999999999898, 2228.849999999999909 ) ) ;
#145=EDGE_CURVE ( 'NONE', #4963, #5906, #6598, .T. ) ;
#207=CARTESIAN_POINT ( 'NONE',  ( -6.349999999999999645, -3578.860000000000127, 2250.998800000000301 ) ) ;
#220=EDGE_CURVE ( 'NONE', #9973, #10014, #6473, .T. ) ;
#230=ORIENTED_EDGE ( 'NONE', *, *, #20185, .F. ) ;
#241=DIRECTION ( 'NONE',  ( 0.000000000000000000, 1.000000000000000000, 0.000000000000000000 ) ) ;
#266=DIRECTION ( 'NONE',  ( 0.000000000000000000, 0.000000000000000000, -1.000000000000000000 ) ) ;
#314=DIRECTION ( 'NONE',  ( 0.000000000000000000, -1.000000000000000000, 0.000000000000000000 ) ) ;
#315=TOROIDAL_SURFACE ( 'NONE', #12233, 3.606799999999999784, 0.7620000000000000107 ) ;
#328=DIRECTION ( 'NONE',  ( 1.000000000000000000, 0.000000000000000000, 0.000000000000000000 ) ) ;
#346=ORIENTED_EDGE ( 'NONE', *, *, #18787, .T. ) ;
#374=DIRECTION ( 'NONE',  ( 0.000000000000000000, 0.000000000000000000, -1.000000000000000000 ) ) ;
#464=AXIS2_PLACEMENT_3D ( 'NONE', #19542, #12397, #1487 ) ;
#472=CARTESIAN_POINT ( 'NONE',  ( -5.588000000000000078, -3694.938000000000102, 2253.487999999999829 ) ) ;
#480=AXIS2_PLACEMENT_3D ( 'NONE', #16637, #2358, #16527 ) ;
#482=AXIS2_PLACEMENT_3D ( 'NONE', #17591, #1542, #8584 ) ;
#498=ADVANCED_FACE ( 'NONE', ( #17092 ), #10062, .T. ) ;
#509=FACE_OUTER_BOUND ( 'NONE', #5261, .T. ) ;
#578=AXIS2_PLACEMENT_3D ( 'NONE', #5509, #9011, #16610 ) ;
#607=DIRECTION ( 'NONE',  ( 0.000000000000000000, 1.000000000000000000, 0.000000000000000000 ) ) ;
#612=ORIENTED_EDGE ( 'NONE', *, *, #10651, .T. ) ;
#628=EDGE_CURVE ( 'NONE', #15285, #22614, #15174, .T. ) ;
#691=EDGE_CURVE ( 'NONE', #20500, #3687, #20338, .T. ) ;
#707=ORIENTED_EDGE ( 'NONE', *, *, #22875, .T. ) ;
#718=CARTESIAN_POINT ( 'NONE',  ( 0.000000000000000000, -3694.938000000000102, 2238.248000000000047 ) ) ;
#739=CARTESIAN_POINT ( 'NONE',  ( 3.048000000000000043, -3694.938000000000102, 2239.009999999999764 ) ) ;
#750=TOROIDAL_SURFACE ( 'NONE', #3747, 3.606799999999999784, 0.7620000000000000107 ) ;
#766=CARTESIAN_POINT ( 'NONE',  ( 0.000000000000000000, -3543.299999999999727, 2254.250000000000000 ) ) ;
#767=VERTEX_POINT ( 'NONE', #4738 ) ;
#770=CARTESIAN_POINT ( 'NONE',  ( 3.810000000000000053, -3694.938000000000102, 2238.248000000000047 ) ) ;
#787=DIRECTION ( 'NONE',  ( 0.000000000000000000, 0.000000000000000000, 1.000000000000000000 ) ) ;
#793=FACE_OUTER_BOUND ( 'NONE', #14812, .T. ) ;
#800=AXIS2_PLACEMENT_3D ( 'NONE', #22482, #19562, #14530 ) ;
#835=AXIS2_PLACEMENT_3D ( 'NONE', #10017, #9888, #2633 ) ;
#842=ORIENTED_EDGE ( 'NONE', *, *, #14098, .T. ) ;
#868=CARTESIAN_POINT ( 'NONE',  ( 0.7620000000000000107, -3695.699999999999818, 2238.248000000000047 ) ) ;
#870=DIRECTION ( 'NONE',  ( 0.000000000000000000, -1.000000000000000000, 0.000000000000000000 ) ) ;
#884=LINE ( 'NONE', #18944, #10321 ) ;
#893=DIRECTION ( 'NONE',  ( 0.000000000000000000, 0.000000000000000000, -1.000000000000000000 ) ) ;
#921=ORIENTED_EDGE ( 'NONE', *, *, #10737, .F. ) ;
#930=DIRECTION ( 'NONE',  ( 0.000000000000000000, 0.000000000000000000, 1.000000000000000000 ) ) ;
#933=CIRCLE ( 'NONE', #10292, 0.7620000000000000107 ) ;
#936=FACE_OUTER_BOUND ( 'NONE', #977, .T. ) ;
#972=ADVANCED_FACE ( 'NONE', ( #509 ), #18315, .T. ) ;
#975=ORIENTED_EDGE ( 'NONE', *, *, #21568, .T. ) ;
#977=EDGE_LOOP ( 'NONE', ( #4447, #15868, #1564, #22394 ) ) ;
#997=AXIS2_PLACEMENT_3D ( 'NONE', #16654, #2817, #607 ) ;
#1000=FACE_BOUND ( 'NONE', #1086, .T. ) ;
#1001=ORIENTED_EDGE ( 'NONE', *, *, #2789, .T. ) ;
#1037=EDGE_CURVE ( 'NONE', #19446, #15888, #18015, .T. ) ;
#1056=SHAPE_DEFINITION_REPRESENTATION ( #8445, #9499 ) ;
#1057=CARTESIAN_POINT ( 'NONE',  ( 3.810000000000000053, -3543.299999999999727, 2228.849999999999909 ) ) ;
#1058=CARTESIAN_POINT ( 'NONE',  ( -5.588000000000000078, -3578.860000000000127, 2247.392000000000280 ) ) ;
#1070=DIRECTION ( 'NONE',  ( 0.000000000000000000, 1.000000000000000000, 0.000000000000000000 ) ) ;
#1086=EDGE_LOOP ( 'NONE', ( #1869, #15862 ) ) ;
#1122=VERTEX_POINT ( 'NONE', #15267 ) ;
#1209=ORIENTED_EDGE ( 'NONE', *, *, #9849, .T. ) ;
#1210=CARTESIAN_POINT ( 'NONE',  ( -5.588000000000000078, -3543.299999999999727, 2229.612000000000080 ) ) ;
#1218=CARTESIAN_POINT ( 'NONE',  ( -5.588000000000000078, -3543.299999999999727, 2253.487999999999829 ) ) ;
#1256=DIRECTION ( 'NONE',  ( 0.000000000000000000, 0.000000000000000000, -1.000000000000000000 ) ) ;
#1274=DIRECTION ( 'NONE',  ( -0.000000000000000000, 1.000000000000000000, 0.000000000000000000 ) ) ;
#1277=EDGE_CURVE ( 'NONE', #8369, #18910, #16516, .T. ) ;
#1295=FACE_OUTER_BOUND ( 'NONE', #3645, .T. ) ;
#1302=ORIENTED_EDGE ( 'NONE', *, *, #2789, .F. ) ;
#1304=DIRECTION ( 'NONE',  ( 0.000000000000000000, 1.000000000000000000, 0.000000000000000000 ) ) ;
#1307=CARTESIAN_POINT ( 'NONE',  ( 3.048000000000000043, -3543.299999999999727, 2238.248000000000047 ) ) ;
#1309=CYLINDRICAL_SURFACE ( 'NONE', #15983, 2.844800000000091700 ) ;
#1338=DIRECTION ( 'NONE',  ( 0.000000000000000000, 1.000000000000000000, 0.000000000000000000 ) ) ;
#1339=CARTESIAN_POINT ( 'NONE',  ( 3.048000000000000043, -3544.061999999999898, 2229.612000000000080 ) ) ;
#1345=ORIENTED_EDGE ( 'NONE', *, *, #16835, .F. ) ;
#1347=DIRECTION ( 'NONE',  ( 1.000000000000000000, 0.000000000000000000, 0.000000000000000000 ) ) ;
#1373=PLANE ( 'NONE',  #11313 ) ;
#1379=CARTESIAN_POINT ( 'NONE',  ( 3.048000000000000043, -3543.299999999999727, 2229.612000000000080 ) ) ;
#1388=DIRECTION ( 'NONE',  ( 0.000000000000000000, 1.000000000000000000, 0.000000000000000000 ) ) ;
#1454=DIRECTION ( 'NONE',  ( 0.000000000000000000, -1.000000000000000000, 0.000000000000000000 ) ) ;
#1475=DIRECTION ( 'NONE',  ( 1.000000000000000000, 0.000000000000000000, 0.000000000000000000 ) ) ;
#1487=DIRECTION ( 'NONE',  ( 0.000000000000000000, -1.000000000000000000, 0.000000000000000000 ) ) ;
#1493=EDGE_CURVE ( 'NONE', #15348, #5042, #16896, .T. ) ;
#1498=PLANE ( 'NONE',  #11810 ) ;
#1500=EDGE_LOOP ( 'NONE', ( #4367, #7166, #13734, #10540 ) ) ;
#1542=DIRECTION ( 'NONE',  ( -1.000000000000000000, 0.000000000000000000, 0.000000000000000000 ) ) ;
#1550=ADVANCED_FACE ( 'NONE', ( #4225 ), #13361, .T. ) ;
#1555=ORIENTED_EDGE ( 'NONE', *, *, #2631, .F. ) ;
#1561=CIRCLE ( 'NONE', #9435, 2.844800000000091700 ) ;
#1564=ORIENTED_EDGE ( 'NONE', *, *, #1037, .T. ) ;
#1575=CYLINDRICAL_SURFACE ( 'NONE', #4354, 0.7620000000000001217 ) ;
#1580=ORIENTED_EDGE ( 'NONE', *, *, #11641, .T. ) ;
#1595=DIRECTION ( 'NONE',  ( 0.000000000000000000, 0.000000000000000000, 1.000000000000000000 ) ) ;
#1596=CIRCLE ( 'NONE', #18805, 0.7619999999999996776 ) ;
#1604=CARTESIAN_POINT ( 'NONE',  ( -5.588000000000000078, -3694.938000000000102, 2229.612000000000080 ) ) ;
#1622=CIRCLE ( 'NONE', #16579, 0.7619999999999294005 ) ;
#1638=DIRECTION ( 'NONE',  ( 0.000000000000000000, -1.000000000000000000, 0.000000000000000000 ) ) ;
#1641=CARTESIAN_POINT ( 'NONE',  ( 3.810000000000000053, -3544.061999999999898, 2229.612000000000080 ) ) ;
#1644=ADVANCED_FACE ( 'NONE', ( #6570 ), #3152, .F. ) ;
#1646=ORIENTED_EDGE ( 'NONE', *, *, #21568, .F. ) ;
#1701=EDGE_CURVE ( 'NONE', #13004, #4281, #19168, .T. ) ;
#1723=VECTOR ( 'NONE', #4700, 1000.000000000000000 ) ;
#1745=CARTESIAN_POINT ( 'NONE',  ( -6.349999999999999645, -3543.299999999999727, 2254.250000000000000 ) ) ;
#1759=PRODUCT_DEFINITION ( 'UNKNOWN', '', #10100, #20731 ) ;
#1802=EDGE_LOOP ( 'NONE', ( #12022, #10512, #21670, #1555 ) ) ;
#1806=EDGE_LOOP ( 'NONE', ( #975, #14282, #10355 ) ) ;
#1808=SPHERICAL_SURFACE ( 'NONE', #21143, 0.7620000000000000107 ) ;
#1816=ORIENTED_EDGE ( 'NONE', *, *, #16841, .T. ) ;
#1836=DIRECTION ( 'NONE',  ( 0.000000000000000000, -1.000000000000000000, 0.000000000000000000 ) ) ;
#1869=ORIENTED_EDGE ( 'NONE', *, *, #21910, .T. ) ;
#1886=EDGE_LOOP ( 'NONE', ( #12243, #7202, #17473, #20445 ) ) ;
#1910=ORIENTED_EDGE ( 'NONE', *, *, #16604, .F. ) ;
#1925=DIRECTION ( 'NONE',  ( 0.000000000000000000, 0.000000000000000000, -1.000000000000000000 ) ) ;
#1928=DIRECTION ( 'NONE',  ( 0.000000000000000000, 0.000000000000000000, 1.000000000000000000 ) ) ;
#1929=ADVANCED_FACE ( 'NONE', ( #7830 ), #5968, .T. ) ;
#1960=EDGE_CURVE ( 'NONE', #20500, #8369, #22528, .T. ) ;
#1974=CARTESIAN_POINT ( 'NONE',  ( 3.048000000000000043, -3695.699999999999818, 2229.612000000000080 ) ) ;
#1990=FACE_OUTER_BOUND ( 'NONE', #22130, .T. ) ;
#2031=ORIENTED_EDGE ( 'NONE', *, *, #4855, .T. ) ;
#2049=VECTOR ( 'NONE', #17052, 1000.000000000000000 ) ;
#2108=VECTOR ( 'NONE', #18026, 1000.000000000000000 ) ;
#2123=FACE_OUTER_BOUND ( 'NONE', #18740, .T. ) ;
#2148=ADVANCED_FACE ( 'NONE', ( #15788 ), #22572, .F. ) ;
#2166=AXIS2_PLACEMENT_3D ( 'NONE', #16151, #10405, #17546 ) ;
#2190=CARTESIAN_POINT ( 'NONE',  ( 3.810000000000000053, -3544.061999999999898, 2229.612000000000080 ) ) ;
#2235=SPHERICAL_SURFACE ( 'NONE', #3193, 0.7620000000000000107 ) ;
#2257=( GEOMETRIC_REPRESENTATION_CONTEXT ( 3 ) GLOBAL_UNCERTAINTY_ASSIGNED_CONTEXT ( ( #16741 ) ) GLOBAL_UNIT_ASSIGNED_CONTEXT ( ( #21126, #3419, #23094 ) ) REPRESENTATION_CONTEXT ( 'NONE', 'WORKASPACE' ) );
#2290=DIRECTION ( 'NONE',  ( 1.000000000000000000, 0.000000000000000000, 0.000000000000000000 ) ) ;
#2309=LINE ( 'NONE', #2751, #10142 ) ;
#2328=DIRECTION ( 'NONE',  ( 0.000000000000000000, 1.000000000000000000, 1.224646799147353207E-16 ) ) ;
#2339=AXIS2_PLACEMENT_3D ( 'NONE', #17308, #1256, #15565 ) ;
#2358=DIRECTION ( 'NONE',  ( -1.000000000000000000, 0.000000000000000000, 0.000000000000000000 ) ) ;
#2423=DIRECTION ( 'NONE',  ( 0.000000000000000000, 1.000000000000000000, 0.000000000000000000 ) ) ;
#2437=CARTESIAN_POINT ( 'NONE',  ( 0.000000000000000000, -3544.061999999999898, 2253.487999999999829 ) ) ;
#2462=VERTEX_POINT ( 'NONE', #22629 ) ;
#2484=SPHERICAL_SURFACE ( 'NONE', #15627, 0.7620000000000000107 ) ;
#2489=ADVANCED_FACE ( 'NONE', ( #13855 ), #14708, .T. ) ;
#2555=ORIENTED_EDGE ( 'NONE', *, *, #21610, .F. ) ;
#2556=EDGE_CURVE ( 'NONE', #20183, #5906, #4586, .T. ) ;
#2557=CARTESIAN_POINT ( 'NONE',  ( 3.810000000000000053, -3694.938000000000102, 2229.612000000000080 ) ) ;
#2574=VERTEX_POINT ( 'NONE', #4947 ) ;
#2575=ORIENTED_EDGE ( 'NONE', *, *, #23095, .F. ) ;
#2589=ORIENTED_EDGE ( 'NONE', *, *, #145, .F. ) ;
#2604=ORIENTED_EDGE ( 'NONE', *, *, #14395, .T. ) ;
#2606=CARTESIAN_POINT ( 'NONE',  ( 0.000000000000000000, 0.000000000000000000, 0.000000000000000000 ) ) ;
#2631=EDGE_CURVE ( 'NONE', #15285, #12671, #1596, .T. ) ;
#2632=DIRECTION ( 'NONE',  ( 0.000000000000000000, 0.000000000000000000, -1.000000000000000000 ) ) ;
#2633=DIRECTION ( 'NONE',  ( 0.000000000000000000, 0.000000000000000000, 1.000000000000000000 ) ) ;
#2661=ORIENTED_EDGE ( 'NONE', *, *, #16841, .F. ) ;
#2671=DIRECTION ( 'NONE',  ( 1.000000000000000000, 0.000000000000000000, 0.000000000000000000 ) ) ;
#2676=EDGE_CURVE ( 'NONE', #19268, #2462, #7590, .T. ) ;
#2703=ORIENTED_EDGE ( 'NONE', *, *, #16004, .T. ) ;
#2746=DIRECTION ( 'NONE',  ( -1.000000000000000000, 0.000000000000000000, 0.000000000000000000 ) ) ;
#2751=CARTESIAN_POINT ( 'NONE',  ( 0.7620000000000000107, -3694.938000000000102, 2239.009999999999764 ) ) ;
#2756=CARTESIAN_POINT ( 'NONE',  ( 3.048000000000000043, -3544.061999999999898, 2238.248000000000047 ) ) ;
#2764=DIRECTION ( 'NONE',  ( 0.000000000000000000, 0.000000000000000000, -1.000000000000000000 ) ) ;
#2789=EDGE_CURVE ( 'NONE', #21067, #15388, #14128, .T. ) ;
#2813=EDGE_LOOP ( 'NONE', ( #17723, #20968, #17350, #19826 ) ) ;
#2817=DIRECTION ( 'NONE',  ( 0.000000000000000000, 0.000000000000000000, 1.000000000000000000 ) ) ;
#2840=DIRECTION ( 'NONE',  ( 1.000000000000000000, 0.000000000000000000, 0.000000000000000000 ) ) ;
#2851=CARTESIAN_POINT ( 'NONE',  ( 0.7620000000000000107, -3543.299999999999727, 2239.771999999999935 ) ) ;
#2857=ORIENTED_EDGE ( 'NONE', *, *, #22697, .T. ) ;
#2948=CARTESIAN_POINT ( 'NONE',  ( -5.588000000000000078, -3578.860000000000127, 2250.236800000000130 ) ) ;
#2969=EDGE_CURVE ( 'NONE', #18582, #5364, #22725, .T. ) ;
#2975=CARTESIAN_POINT ( 'NONE',  ( -6.349999999999999645, -3694.938000000000102, 2253.487999999999829 ) ) ;
#2982=CYLINDRICAL_SURFACE ( 'NONE', #20340, 0.7619999999999996776 ) ;
#2990=CIRCLE ( 'NONE', #4843, 0.7619999999999294005 ) ;
#2992=DIRECTION ( 'NONE',  ( 0.000000000000000000, 0.000000000000000000, -1.000000000000000000 ) ) ;
#3015=EDGE_LOOP ( 'NONE', ( #14055, #14205, #21740, #14609 ) ) ;
#3058=CARTESIAN_POINT ( 'NONE',  ( -0.7620000000000000107, -3544.061999999999898, 2254.250000000000000 ) ) ;
#3068=DIRECTION ( 'NONE',  ( 0.000000000000000000, 1.000000000000000000, -1.224646799147353207E-16 ) ) ;
#3081=CIRCLE ( 'NONE', #464, 0.7619999999999294005 ) ;
#3116=CLOSED_SHELL ( 'NONE', ( #17229, #11564, #20533, #5705, #12324, #6964, #9811, #8551, #16932, #2489, #13835, #7641, #4021, #6800, #9019, #16453, #5515, #1929, #15278, #8418, #13537, #5023, #16532, #11114, #14265, #19609, #1550, #972, #22940, #1644, #19187, #13238, #14899, #8861, #9921, #14180, #5377, #4836, #5387, #11084, #22107, #498, #6391, #9132, #15882, #12707, #21413, #3800, #8097, #2148 ) ) ;
#3121=CARTESIAN_POINT ( 'NONE',  ( 3.048000000000000043, -3544.061999999999898, 2238.248000000000047 ) ) ;
#3152=PLANE ( 'NONE',  #20294 ) ;
#3162=DIRECTION ( 'NONE',  ( 1.000000000000000000, 0.000000000000000000, 0.000000000000000000 ) ) ;
#3165=DIRECTION ( 'NONE',  ( -1.000000000000000000, 0.000000000000000000, 0.000000000000000000 ) ) ;
#3193=AXIS2_PLACEMENT_3D ( 'NONE', #472, #7614, #14773 ) ;
#3209=AXIS2_PLACEMENT_3D ( 'NONE', #13325, #9580, #6308 ) ;
#3219=EDGE_CURVE ( 'NONE', #11141, #5364, #14845, .T. ) ;
#3228=DIRECTION ( 'NONE',  ( -1.000000000000000000, 0.000000000000000000, 0.000000000000000000 ) ) ;
#3329=CARTESIAN_POINT ( 'NONE',  ( 0.000000000000000000, -3578.860000000000127, 2243.785200000000259 ) ) ;
#3338=CARTESIAN_POINT ( 'NONE',  ( -5.588000000000000078, -3544.061999999999898, 2253.487999999999829 ) ) ;
#3367=DIRECTION ( 'NONE',  ( 1.000000000000000000, 0.000000000000000000, 0.000000000000000000 ) ) ;
#3383=CIRCLE ( 'NONE', #19483, 0.7620000000000001217 ) ;
#3392=ORIENTED_EDGE ( 'NONE', *, *, #22743, .T. ) ;
#3419=( NAMED_UNIT ( * ) PLANE_ANGLE_UNIT ( ) SI_UNIT ( $, .RADIAN. ) );
#3440=EDGE_LOOP ( 'NONE', ( #3392, #17178, #6717, #10395 ) ) ;
#3479=DIRECTION ( 'NONE',  ( -1.000000000000000000, 0.000000000000000000, 0.000000000000000000 ) ) ;
#3495=CARTESIAN_POINT ( 'NONE',  ( -5.588000000000000078, -3544.061999999999898, 2254.250000000000000 ) ) ;
#3513=CARTESIAN_POINT ( 'NONE',  ( 0.000000000000000000, -3544.061999999999898, 2239.771999999999935 ) ) ;
#3541=EDGE_CURVE ( 'NONE', #12671, #15650, #21955, .T. ) ;
#3574=DIRECTION ( 'NONE',  ( 1.000000000000000000, 0.000000000000000000, 0.000000000000000000 ) ) ;
#3619=ORIENTED_EDGE ( 'NONE', *, *, #2676, .T. ) ;
#3627=CARTESIAN_POINT ( 'NONE',  ( -0.7620000000000000107, -3544.061999999999898, 2254.250000000000000 ) ) ;
#3645=EDGE_LOOP ( 'NONE', ( #13445, #11800, #11607, #22995 ) ) ;
#3668=ORIENTED_EDGE ( 'NONE', *, *, #7698, .T. ) ;
#3676=FACE_OUTER_BOUND ( 'NONE', #2813, .T. ) ;
#3687=VERTEX_POINT ( 'NONE', #18070 ) ;
#3700=VECTOR ( 'NONE', #8059, 1000.000000000000000 ) ;
#3711=AXIS2_PLACEMENT_3D ( 'NONE', #766, #20463, #4411 ) ;
#3713=CARTESIAN_POINT ( 'NONE',  ( 0.000000000000000000, -3660.140000000000327, 2243.785200000000259 ) ) ;
#3714=CARTESIAN_POINT ( 'NONE',  ( 0.000000000000000000, -3694.938000000000102, 2253.487999999999829 ) ) ;
#3715=CIRCLE ( 'NONE', #16809, 0.7619999999999294005 ) ;
#3719=CARTESIAN_POINT ( 'NONE',  ( -5.588000000000000078, -3660.140000000000327, 2247.392000000000280 ) ) ;
#3747=AXIS2_PLACEMENT_3D ( 'NONE', #11032, #16309, #266 ) ;
#3800=ADVANCED_FACE ( 'NONE', ( #11493 ), #2484, .T. ) ;
#3809=DIRECTION ( 'NONE',  ( -1.000000000000000000, 0.000000000000000000, 0.000000000000000000 ) ) ;
#3849=VERTEX_POINT ( 'NONE', #4012 ) ;
#3858=AXIS2_PLACEMENT_3D ( 'NONE', #13500, #20528, #6143 ) ;
#3876=AXIS2_PLACEMENT_3D ( 'NONE', #21562, #3974, #18264 ) ;
#3968=CIRCLE ( 'NONE', #8475, 0.7620000000000000107 ) ;
#3972=CIRCLE ( 'NONE', #13318, 0.7620000000000001217 ) ;
#3974=DIRECTION ( 'NONE',  ( 0.000000000000000000, 1.000000000000000000, 0.000000000000000000 ) ) ;
#4007=EDGE_LOOP ( 'NONE', ( #9677, #16560, #13283, #14138 ) ) ;
#4011=AXIS2_PLACEMENT_3D ( 'NONE', #10454, #19017, #23096 ) ;
#4012=CARTESIAN_POINT ( 'NONE',  ( -0.7620000000000000107, -3578.860000000000127, 2244.547199999999975 ) ) ;
#4018=AXIS2_PLACEMENT_3D ( 'NONE', #18520, #20616, #930 ) ;
#4021=ADVANCED_FACE ( 'NONE', ( #13605 ), #22731, .T. ) ;
#4054=DIRECTION ( 'NONE',  ( 1.000000000000000000, 0.000000000000000000, 0.000000000000000000 ) ) ;
#4090=CIRCLE ( 'NONE', #22045, 3.606800000000021100 ) ;
#4109=EDGE_LOOP ( 'NONE', ( #4560, #5563 ) ) ;
#4111=CYLINDRICAL_SURFACE ( 'NONE', #480, 2.844800000000091700 ) ;
#4121=LINE ( 'NONE', #4659, #14692 ) ;
#4125=CARTESIAN_POINT ( 'NONE',  ( -5.588000000000000078, -3578.860000000000127, 2247.392000000000280 ) ) ;
#4130=EDGE_LOOP ( 'NONE', ( #612, #14052, #8881, #4584 ) ) ;
#4156=CYLINDRICAL_SURFACE ( 'NONE', #9597, 0.7620000000000000107 ) ;
#4177=AXIS2_PLACEMENT_3D ( 'NONE', #9418, #16557, #7649 ) ;
#4211=CARTESIAN_POINT ( 'NONE',  ( -0.7620000000000000107, -3578.860000000000127, 2250.236800000000130 ) ) ;
#4225=FACE_OUTER_BOUND ( 'NONE', #1802, .T. ) ;
#4230=AXIS2_PLACEMENT_3D ( 'NONE', #7624, #19827, #12676 ) ;
#4241=DIRECTION ( 'NONE',  ( 0.000000000000000000, 0.000000000000000000, 1.000000000000000000 ) ) ;
#4281=VERTEX_POINT ( 'NONE', #20370 ) ;
#4282=DIRECTION ( 'NONE',  ( 1.000000000000000000, 0.000000000000000000, 0.000000000000000000 ) ) ;
#4318=AXIS2_PLACEMENT_3D ( 'NONE', #11732, #5909, #16779 ) ;
#4350=DIRECTION ( 'NONE',  ( 0.000000000000000000, 1.000000000000000000, 0.000000000000000000 ) ) ;
#4354=AXIS2_PLACEMENT_3D ( 'NONE', #23126, #6986, #8736 ) ;
#4365=ORIENTED_EDGE ( 'NONE', *, *, #14237, .T. ) ;
#4367=ORIENTED_EDGE ( 'NONE', *, *, #10353, .T. ) ;
#4368=ORIENTED_EDGE ( 'NONE', *, *, #7698, .F. ) ;
#4376=EDGE_CURVE ( 'NONE', #3687, #18263, #2990, .T. ) ;
#4378=CARTESIAN_POINT ( 'NONE',  ( -5.588000000000000078, -3543.299999999999727, 2229.612000000000080 ) ) ;
#4401=DIRECTION ( 'NONE',  ( 1.000000000000000000, 0.000000000000000000, 0.000000000000000000 ) ) ;
#4411=DIRECTION ( 'NONE',  ( 0.000000000000000000, 0.000000000000000000, 1.000000000000000000 ) ) ;
#4423=ORIENTED_EDGE ( 'NONE', *, *, #12597, .F. ) ;
#4447=ORIENTED_EDGE ( 'NONE', *, *, #15005, .F. ) ;
#4458=CARTESIAN_POINT ( 'NONE',  ( 0.7620000000000000107, -3694.938000000000102, 2239.771999999999935 ) ) ;
#4481=( GEOMETRIC_REPRESENTATION_CONTEXT ( 3 ) GLOBAL_UNCERTAINTY_ASSIGNED_CONTEXT ( ( #17837 ) ) GLOBAL_UNIT_ASSIGNED_CONTEXT ( ( #13621, #15622, #17129 ) ) REPRESENTATION_CONTEXT ( 'NONE', 'WORKASPACE' ) );
#4519=DIRECTION ( 'NONE',  ( 0.000000000000000000, 0.000000000000000000, -1.000000000000000000 ) ) ;
#4559=VERTEX_POINT ( 'NONE', #3713 ) ;
#4560=ORIENTED_EDGE ( 'NONE', *, *, #13323, .T. ) ;
#4578=DIRECTION ( 'NONE',  ( -1.000000000000000000, 0.000000000000000000, 0.000000000000000000 ) ) ;
#4584=ORIENTED_EDGE ( 'NONE', *, *, #2556, .F. ) ;
#4586=CIRCLE ( 'NONE', #18443, 0.7620000000000000107 ) ;
#4610=EDGE_CURVE ( 'NONE', #1122, #8369, #16149, .T. ) ;
#4615=CARTESIAN_POINT ( 'NONE',  ( -5.588000000000000078, -3543.299999999999727, 2229.612000000000080 ) ) ;
#4618=DIRECTION ( 'NONE',  ( 0.000000000000000000, 0.000000000000000000, -1.000000000000000000 ) ) ;
#4629=ORIENTED_EDGE ( 'NONE', *, *, #18562, .T. ) ;
#4632=FACE_OUTER_BOUND ( 'NONE', #9124, .T. ) ;
#4651=CARTESIAN_POINT ( 'NONE',  ( 3.810000000000000053, -3543.299999999999727, 2239.009999999999764 ) ) ;
#4659=CARTESIAN_POINT ( 'NONE',  ( 3.048000000000000043, -3544.061999999999898, 2239.009999999999764 ) ) ;
#4668=ORIENTED_EDGE ( 'NONE', *, *, #15590, .F. ) ;
#4682=EDGE_LOOP ( 'NONE', ( #6133, #20929, #18050 ) ) ;
#4685=DIRECTION ( 'NONE',  ( 0.000000000000000000, 0.000000000000000000, -1.000000000000000000 ) ) ;
#4700=DIRECTION ( 'NONE',  ( 0.000000000000000000, -1.000000000000000000, 0.000000000000000000 ) ) ;
#4729=AXIS2_PLACEMENT_3D ( 'NONE', #13322, #17055, #2764 ) ;
#4738=CARTESIAN_POINT ( 'NONE',  ( 0.7619999999998999796, -3695.699999999999818, 2238.248000000000047 ) ) ;
#4740=TOROIDAL_SURFACE ( 'NONE', #7745, 3.606799999999999784, 0.7620000000000000107 ) ;
#4753=AXIS2_PLACEMENT_3D ( 'NONE', #12423, #7607, #14420 ) ;
#4792=CARTESIAN_POINT ( 'NONE',  ( -6.349999999999999645, -3543.299999999999727, 2228.849999999999909 ) ) ;
#4799=ORIENTED_EDGE ( 'NONE', *, *, #23021, .T. ) ;
#4814=CARTESIAN_POINT ( 'NONE',  ( -6.349999999999999645, -3694.938000000000102, 2253.487999999999829 ) ) ;
#4822=DIRECTION ( 'NONE',  ( 1.000000000000000000, 0.000000000000000000, 0.000000000000000000 ) ) ;
#4836=ADVANCED_FACE ( 'NONE', ( #10140, #1000, #4632 ), #22672, .F. ) ;
#4843=AXIS2_PLACEMENT_3D ( 'NONE', #10284, #10167, #11572 ) ;
#4854=CARTESIAN_POINT ( 'NONE',  ( -5.588000000000000078, -3543.299999999999727, 2253.487999999999829 ) ) ;
#4855=EDGE_CURVE ( 'NONE', #18606, #18582, #8163, .T. ) ;
#4899=DIRECTION ( 'NONE',  ( 0.000000000000000000, 0.000000000000000000, -1.000000000000000000 ) ) ;
#4942=CIRCLE ( 'NONE', #19924, 0.7619999999999294005 ) ;
#4947=CARTESIAN_POINT ( 'NONE',  ( 0.000000000000000000, -3578.860000000000127, 2250.998800000000301 ) ) ;
#4959=ORIENTED_EDGE ( 'NONE', *, *, #18982, .F. ) ;
#4963=VERTEX_POINT ( 'NONE', #19053 ) ;
#4975=EDGE_CURVE ( 'NONE', #2462, #7518, #5231, .T. ) ;
#4997=AXIS2_PLACEMENT_3D ( 'NONE', #9954, #4685, #20228 ) ;
#5005=ORIENTED_EDGE ( 'NONE', *, *, #16424, .F. ) ;
#5007=CARTESIAN_POINT ( 'NONE',  ( -5.588000000000000078, -3544.061999999999898, 2253.487999999999829 ) ) ;
#5023=ADVANCED_FACE ( 'NONE', ( #19515 ), #19288, .T. ) ;
#5042=VERTEX_POINT ( 'NONE', #12132 ) ;
#5056=VECTOR ( 'NONE', #21891, 1000.000000000000000 ) ;
#5088=EDGE_CURVE ( 'NONE', #12135, #18858, #20199, .T. ) ;
#5102=DIRECTION ( 'NONE',  ( 1.000000000000000000, 0.000000000000000000, 0.000000000000000000 ) ) ;
#5140=DIRECTION ( 'NONE',  ( 0.000000000000000000, -1.000000000000000000, 0.000000000000000000 ) ) ;
#5147=DIRECTION ( 'NONE',  ( 0.000000000000000000, -1.000000000000000000, 0.000000000000000000 ) ) ;
#5151=ORIENTED_EDGE ( 'NONE', *, *, #15590, .T. ) ;
#5174=FACE_OUTER_BOUND ( 'NONE', #14553, .T. ) ;
#5187=ORIENTED_EDGE ( 'NONE', *, *, #9849, .F. ) ;
#5221=VECTOR ( 'NONE', #8501, 1000.000000000000000 ) ;
#5231=CIRCLE ( 'NONE', #5608, 0.7620000000000001217 ) ;
#5238=SPHERICAL_SURFACE ( 'NONE', #5793, 0.7620000000000000107 ) ;
#5240=DIRECTION ( 'NONE',  ( -1.000000000000000000, 0.000000000000000000, 0.000000000000000000 ) ) ;
#5255=CARTESIAN_POINT ( 'NONE',  ( -0.7620000000000000107, -3543.299999999999727, 2253.487999999999829 ) ) ;
#5261=EDGE_LOOP ( 'NONE', ( #12924, #16494, #2857 ) ) ;
#5303=CARTESIAN_POINT ( 'NONE',  ( 3.048000000000000043, -3694.938000000000102, 2229.612000000000080 ) ) ;
#5335=ORIENTED_EDGE ( 'NONE', *, *, #15682, .F. ) ;
#5340=AXIS2_PLACEMENT_3D ( 'NONE', #1379, #13812, #3367 ) ;
#5342=DIRECTION ( 'NONE',  ( 1.000000000000000000, 0.000000000000000000, 0.000000000000000000 ) ) ;
#5364=VERTEX_POINT ( 'NONE', #6495 ) ;
#5371=DIRECTION ( 'NONE',  ( -1.000000000000000000, 0.000000000000000000, 0.000000000000000000 ) ) ;
#5377=ADVANCED_FACE ( 'NONE', ( #11748 ), #18904, .F. ) ;
#5387=ADVANCED_FACE ( 'NONE', ( #8681 ), #6034, .T. ) ;
#5399=AXIS2_PLACEMENT_3D ( 'NONE', #3719, #328, #21881 ) ;
#5509=CARTESIAN_POINT ( 'NONE',  ( 1.270000000000000018, -3660.140000000000327, 2247.392000000000280 ) ) ;
#5515=ADVANCED_FACE ( 'NONE', ( #5174 ), #19808, .T. ) ;
#5563=ORIENTED_EDGE ( 'NONE', *, *, #10070, .T. ) ;
#5570=DIRECTION ( 'NONE',  ( -1.000000000000000000, 0.000000000000000000, 0.000000000000000000 ) ) ;
#5572=CARTESIAN_POINT ( 'NONE',  ( 0.000000000000000000, -3544.061999999999898, 2253.487999999999829 ) ) ;
#5583=FACE_OUTER_BOUND ( 'NONE', #22416, .T. ) ;
#5598=AXIS2_PLACEMENT_3D ( 'NONE', #5830, #4054, #18578 ) ;
#5608=AXIS2_PLACEMENT_3D ( 'NONE', #2756, #12367, #10728 ) ;
#5611=AXIS2_PLACEMENT_3D ( 'NONE', #2606, #9751, #7545 ) ;
#5628=VERTEX_POINT ( 'NONE', #4211 ) ;
#5635=DIRECTION ( 'NONE',  ( 1.000000000000000000, 0.000000000000000000, 0.000000000000000000 ) ) ;
#5652=CARTESIAN_POINT ( 'NONE',  ( -0.7620000000000000107, -3660.140000000000327, 2250.998800000000301 ) ) ;
#5655=CARTESIAN_POINT ( 'NONE',  ( -5.588000000000000078, -3578.860000000000127, 2243.785200000000259 ) ) ;
#5666=ORIENTED_EDGE ( 'NONE', *, *, #4610, .F. ) ;
#5705=ADVANCED_FACE ( 'NONE', ( #793 ), #4740, .T. ) ;
#5710=TOROIDAL_SURFACE ( 'NONE', #19178, 3.606799999999999784, 0.7620000000000000107 ) ;
#5712=CARTESIAN_POINT ( 'NONE',  ( -6.349999999999999645, -3694.938000000000102, 2229.612000000000080 ) ) ;
#5715=AXIS2_PLACEMENT_3D ( 'NONE', #5655, #12790, #374 ) ;
#5734=AXIS2_PLACEMENT_3D ( 'NONE', #1339, #19395, #19276 ) ;
#5793=AXIS2_PLACEMENT_3D ( 'NONE', #3121, #12381, #1475 ) ;
#5820=CARTESIAN_POINT ( 'NONE',  ( -5.588000000000000078, -3694.938000000000102, 2253.487999999999829 ) ) ;
#5830=CARTESIAN_POINT ( 'NONE',  ( 3.048000000000000043, -3694.938000000000102, 2238.248000000000047 ) ) ;
#5860=AXIS2_PLACEMENT_3D ( 'NONE', #22195, #13298, #23121 ) ;
#5865=ORIENTED_EDGE ( 'NONE', *, *, #22712, .T. ) ;
#5879=ORIENTED_EDGE ( 'NONE', *, *, #16835, .T. ) ;
#5900=CARTESIAN_POINT ( 'NONE',  ( 3.048000000000000043, -3543.299999999999727, 2238.248000000000047 ) ) ;
#5906=VERTEX_POINT ( 'NONE', #5255 ) ;
#5909=DIRECTION ( 'NONE',  ( 0.000000000000000000, 0.000000000000000000, -1.000000000000000000 ) ) ;
#5948=ORIENTED_EDGE ( 'NONE', *, *, #10431, .F. ) ;
#5968=CYLINDRICAL_SURFACE ( 'NONE', #21063, 0.7619999999999294005 ) ;
#5973=EDGE_CURVE ( 'NONE', #1122, #3687, #20482, .T. ) ;
#6029=ADVANCED_BREP_SHAPE_REPRESENTATION ( '', ( #21083, #5611 ), #4481 ) ;
#6034=CYLINDRICAL_SURFACE ( 'NONE', #7052, 0.7620000000000000107 ) ;
#6037=EDGE_LOOP ( 'NONE', ( #2031, #4368, #6948, #5005 ) ) ;
#6039=CYLINDRICAL_SURFACE ( 'NONE', #11403, 0.7619999999999294005 ) ;
#6044=VECTOR ( 'NONE', #4282, 1000.000000000000000 ) ;
#6074=ORIENTED_EDGE ( 'NONE', *, *, #1037, .F. ) ;
#6102=DIRECTION ( 'NONE',  ( 0.000000000000000000, 0.000000000000000000, -1.000000000000000000 ) ) ;
#6132=VECTOR ( 'NONE', #22741, 1000.000000000000000 ) ;
#6133=ORIENTED_EDGE ( 'NONE', *, *, #20896, .T. ) ;
#6143=DIRECTION ( 'NONE',  ( 0.000000000000000000, 0.000000000000000000, 1.000000000000000000 ) ) ;
#6154=EDGE_LOOP ( 'NONE', ( #1302, #1209, #8297, #15186 ) ) ;
#6155=LINE ( 'NONE', #14943, #22991 ) ;
#6156=FACE_OUTER_BOUND ( 'NONE', #1500, .T. ) ;
#6163=EDGE_CURVE ( 'NONE', #3849, #5628, #8094, .T. ) ;
#6193=CARTESIAN_POINT ( 'NONE',  ( 3.810000000000000053, -3544.061999999999898, 2238.248000000000047 ) ) ;
#6205=TOROIDAL_SURFACE ( 'NONE', #18924, 3.606799999999999784, 0.7620000000000000107 ) ;
#6223=VECTOR ( 'NONE', #10871, 1000.000000000000000 ) ;
#6225=ORIENTED_EDGE ( 'NONE', *, *, #2631, .T. ) ;
#6226=DIRECTION ( 'NONE',  ( 0.000000000000000000, 0.000000000000000000, 1.000000000000000000 ) ) ;
#6239=DIRECTION ( 'NONE',  ( 1.000000000000000000, 0.000000000000000000, 0.000000000000000000 ) ) ;
#6244=ORIENTED_EDGE ( 'NONE', *, *, #14237, .F. ) ;
#6283=DIRECTION ( 'NONE',  ( 0.000000000000000000, -1.000000000000000000, 0.000000000000000000 ) ) ;
#6297=CARTESIAN_POINT ( 'NONE',  ( 3.048000000000000043, -3695.699999999999818, 2238.248000000000047 ) ) ;
#6308=DIRECTION ( 'NONE',  ( -1.000000000000000000, 0.000000000000000000, 0.000000000000000000 ) ) ;
#6315=DIRECTION ( 'NONE',  ( 0.000000000000000000, 1.000000000000000000, 0.000000000000000000 ) ) ;
#6324=AXIS2_PLACEMENT_3D ( 'NONE', #21617, #5570, #16218 ) ;
#6347=EDGE_LOOP ( 'NONE', ( #14225, #17, #14345, #13794 ) ) ;
#6358=CARTESIAN_POINT ( 'NONE',  ( -6.349999999999999645, -3544.061999999999898, 2253.487999999999829 ) ) ;
#6389=ORIENTED_EDGE ( 'NONE', *, *, #13504, .F. ) ;
#6391=ADVANCED_FACE ( 'NONE', ( #6995 ), #4156, .T. ) ;
#6394=LINE ( 'NONE', #20917, #5221 ) ;
#6421=CARTESIAN_POINT ( 'NONE',  ( 3.048000000000000043, -3543.299999999999727, 2238.248000000000047 ) ) ;
#6427=EDGE_CURVE ( 'NONE', #18679, #22455, #6987, .T. ) ;
#6466=DIRECTION ( 'NONE',  ( 0.000000000000000000, 0.000000000000000000, 1.000000000000000000 ) ) ;
#6473=LINE ( 'NONE', #3058, #10991 ) ;
#6486=CARTESIAN_POINT ( 'NONE',  ( -5.588000000000000078, -3544.061999999999898, 2228.849999999999909 ) ) ;
#6492=CIRCLE ( 'NONE', #3858, 0.7619999999999294005 ) ;
#6495=CARTESIAN_POINT ( 'NONE',  ( -5.588000000000000078, -3695.699999999999818, 2229.612000000000080 ) ) ;
#6499=ORIENTED_EDGE ( 'NONE', *, *, #2969, .F. ) ;
#6516=CARTESIAN_POINT ( 'NONE',  ( 0.7620000000000000107, -3694.938000000000102, 2238.248000000000047 ) ) ;
#6519=EDGE_LOOP ( 'NONE', ( #10032, #9595, #3668 ) ) ;
#6542=VECTOR ( 'NONE', #10387, 1000.000000000000000 ) ;
#6570=FACE_OUTER_BOUND ( 'NONE', #11753, .T. ) ;
#6576=EDGE_CURVE ( 'NONE', #8944, #19446, #11750, .T. ) ;
#6598=LINE ( 'NONE', #13737, #6132 ) ;
#6601=VECTOR ( 'NONE', #8323, 1000.000000000000000 ) ;
#6612=CARTESIAN_POINT ( 'NONE',  ( 1.270000000000000018, -3660.140000000000327, 2247.392000000000280 ) ) ;
#6635=CARTESIAN_POINT ( 'NONE',  ( 3.048000000000000043, -3544.061999999999898, 2238.248000000000047 ) ) ;
#6666=ORIENTED_EDGE ( 'NONE', *, *, #2556, .T. ) ;
#6693=EDGE_LOOP ( 'NONE', ( #19902, #4959, #19260, #20104 ) ) ;
#6696=CARTESIAN_POINT ( 'NONE',  ( -0.7619999999998999796, -3695.699999999999818, 2239.771999999999935 ) ) ;
#6705=CARTESIAN_POINT ( 'NONE',  ( -0.7620000000000000107, -3660.140000000000327, 2247.392000000000280 ) ) ;
#6717=ORIENTED_EDGE ( 'NONE', *, *, #6576, .T. ) ;
#6771=CARTESIAN_POINT ( 'NONE',  ( -6.349999999999999645, -3544.061999999999898, 2229.612000000000080 ) ) ;
#6783=CYLINDRICAL_SURFACE ( 'NONE', #2339, 0.7619999999999996776 ) ;
#6787=CARTESIAN_POINT ( 'NONE',  ( -0.7620000000000000107, -3694.938000000000102, 2253.487999999999829 ) ) ;
#6792=FACE_OUTER_BOUND ( 'NONE', #7532, .T. ) ;
#6799=AXIS2_PLACEMENT_3D ( 'NONE', #23087, #7064, #13972 ) ;
#6800=ADVANCED_FACE ( 'NONE', ( #8488 ), #19731, .T. ) ;
#6852=ORIENTED_EDGE ( 'NONE', *, *, #22718, .T. ) ;
#6864=PLANE ( 'NONE',  #10954 ) ;
#6872=DIRECTION ( 'NONE',  ( 0.000000000000000000, 0.000000000000000000, -1.000000000000000000 ) ) ;
#6930=EDGE_CURVE ( 'NONE', #14398, #15285, #11605, .T. ) ;
#6948=ORIENTED_EDGE ( 'NONE', *, *, #15136, .T. ) ;
#6964=ADVANCED_FACE ( 'NONE', ( #12429 ), #6205, .T. ) ;
#6986=DIRECTION ( 'NONE',  ( 0.000000000000000000, 0.000000000000000000, -1.000000000000000000 ) ) ;
#6987=CIRCLE ( 'NONE', #16716, 0.7619999999999294005 ) ;
#6988=EDGE_LOOP ( 'NONE', ( #5879, #13488 ) ) ;
#6995=FACE_OUTER_BOUND ( 'NONE', #4130, .T. ) ;
#7014=ORIENTED_EDGE ( 'NONE', *, *, #22875, .F. ) ;
#7016=CIRCLE ( 'NONE', #4753, 3.606800000000021100 ) ;
#7040=ORIENTED_EDGE ( 'NONE', *, *, #8524, .T. ) ;
#7052=AXIS2_PLACEMENT_3D ( 'NONE', #13168, #1638, #12543 ) ;
#7064=DIRECTION ( 'NONE',  ( 0.000000000000000000, 1.000000000000000000, 0.000000000000000000 ) ) ;
#7068=FACE_OUTER_BOUND ( 'NONE', #6154, .T. ) ;
#7086=VERTEX_POINT ( 'NONE', #9270 ) ;
#7088=CARTESIAN_POINT ( 'NONE',  ( -0.7620000000000000107, -3694.938000000000102, 2253.487999999999829 ) ) ;
#7101=CARTESIAN_POINT ( 'NONE',  ( 0.000000000000000000, -3578.860000000000127, 2247.392000000000280 ) ) ;
#7109=AXIS2_PLACEMENT_3D ( 'NONE', #15294, #11894, #17507 ) ;
#7114=FACE_OUTER_BOUND ( 'NONE', #10937, .T. ) ;
#7140=LINE ( 'NONE', #16044, #14048 ) ;
#7166=ORIENTED_EDGE ( 'NONE', *, *, #22299, .T. ) ;
#7176=DIRECTION ( 'NONE',  ( 0.000000000000000000, 0.000000000000000000, -1.000000000000000000 ) ) ;
#7184=ORIENTED_EDGE ( 'NONE', *, *, #7931, .F. ) ;
#7194=AXIS2_PLACEMENT_3D ( 'NONE', #9726, #6226, #15011 ) ;
#7202=ORIENTED_EDGE ( 'NONE', *, *, #4376, .F. ) ;
#7207=VECTOR ( 'NONE', #5342, 1000.000000000000000 ) ;
#7226=CYLINDRICAL_SURFACE ( 'NONE', #19263, 2.844800000000091700 ) ;
#7246=DIRECTION ( 'NONE',  ( -1.000000000000000000, 0.000000000000000000, 0.000000000000000000 ) ) ;
#7290=DIRECTION ( 'NONE',  ( 0.000000000000000000, 0.000000000000000000, -1.000000000000000000 ) ) ;
#7299=EDGE_LOOP ( 'NONE', ( #15669, #1580, #5187, #19780 ) ) ;
#7331=ORIENTED_EDGE ( 'NONE', *, *, #12597, .T. ) ;
#7458=LINE ( 'NONE', #2190, #9568 ) ;
#7505=EDGE_CURVE ( 'NONE', #11737, #7086, #17600, .T. ) ;
#7518=VERTEX_POINT ( 'NONE', #1307 ) ;
#7532=EDGE_LOOP ( 'NONE', ( #19207, #13120, #8666, #13637 ) ) ;
#7545=DIRECTION ( 'NONE',  ( 1.000000000000000000, 0.000000000000000000, 0.000000000000000000 ) ) ;
#7553=DIRECTION ( 'NONE',  ( 0.000000000000000000, 0.000000000000000000, 1.000000000000000000 ) ) ;
#7566=AXIS2_PLACEMENT_3D ( 'NONE', #7101, #16230, #12831 ) ;
#7580=CARTESIAN_POINT ( 'NONE',  ( 1.270000000000000018, -3660.140000000000327, 2244.547199999999975 ) ) ;
#7583=EDGE_CURVE ( 'NONE', #22749, #22295, #16486, .T. ) ;
#7590=CIRCLE ( 'NONE', #4230, 0.7619999999999294005 ) ;
#7607=DIRECTION ( 'NONE',  ( 1.000000000000000000, 0.000000000000000000, 0.000000000000000000 ) ) ;
#7614=DIRECTION ( 'NONE',  ( 0.000000000000000000, 1.000000000000000000, 0.000000000000000000 ) ) ;
#7624=CARTESIAN_POINT ( 'NONE',  ( 3.048000000000000043, -3544.061999999999898, 2238.248000000000047 ) ) ;
#7641=ADVANCED_FACE ( 'NONE', ( #7068 ), #750, .T. ) ;
#7649=DIRECTION ( 'NONE',  ( 1.000000000000000000, 0.000000000000000000, 0.000000000000000000 ) ) ;
#7669=CARTESIAN_POINT ( 'NONE',  ( -5.588000000000000078, -3660.140000000000327, 2243.785200000000259 ) ) ;
#7698=EDGE_CURVE ( 'NONE', #4281, #18582, #3383, .T. ) ;
#7715=DIRECTION ( 'NONE',  ( 0.000000000000000000, 0.000000000000000000, 1.000000000000000000 ) ) ;
#7745=AXIS2_PLACEMENT_3D ( 'NONE', #18721, #2671, #4899 ) ;
#7772=AXIS2_PLACEMENT_3D ( 'NONE', #12534, #241, #23070 ) ;
#7802=EDGE_CURVE ( 'NONE', #15650, #15285, #22095, .T. ) ;
#7806=CARTESIAN_POINT ( 'NONE',  ( -5.588000000000000078, -3694.938000000000102, 2229.612000000000080 ) ) ;
#7817=VERTEX_POINT ( 'NONE', #14272 ) ;
#7830=FACE_OUTER_BOUND ( 'NONE', #3015, .T. ) ;
#7833=VECTOR ( 'NONE', #2992, 1000.000000000000000 ) ;
#7835=EDGE_CURVE ( 'NONE', #4963, #8499, #15099, .T. ) ;
#7871=DIRECTION ( 'NONE',  ( 1.000000000000000000, 0.000000000000000000, 0.000000000000000000 ) ) ;
#7897=FACE_OUTER_BOUND ( 'NONE', #18768, .T. ) ;
#7904=DIRECTION ( 'NONE',  ( 1.000000000000000000, 0.000000000000000000, 0.000000000000000000 ) ) ;
#7931=EDGE_CURVE ( 'NONE', #22749, #19266, #21844, .T. ) ;
#7941=EDGE_CURVE ( 'NONE', #767, #19446, #1622, .T. ) ;
#7956=CIRCLE ( 'NONE', #14319, 3.606800000000021100 ) ;
#8006=CIRCLE ( 'NONE', #18470, 0.7619999999999294005 ) ;
#8015=CARTESIAN_POINT ( 'NONE',  ( 0.000000000000000000, -3694.938000000000102, 2239.771999999999935 ) ) ;
#8031=LINE ( 'NONE', #868, #14573 ) ;
#8059=DIRECTION ( 'NONE',  ( 0.000000000000000000, 0.000000000000000000, -1.000000000000000000 ) ) ;
#8091=VERTEX_POINT ( 'NONE', #3329 ) ;
#8094=CIRCLE ( 'NONE', #12961, 2.844800000000091700 ) ;
#8097=ADVANCED_FACE ( 'NONE', ( #10480 ), #1575, .T. ) ;
#8108=FACE_OUTER_BOUND ( 'NONE', #9184, .T. ) ;
#8145=AXIS2_PLACEMENT_3D ( 'NONE', #1057, #13838, #3162 ) ;
#8151=CYLINDRICAL_SURFACE ( 'NONE', #7109, 0.7619999999999294005 ) ;
#8154=DIRECTION ( 'NONE',  ( 0.000000000000000000, 0.000000000000000000, -1.000000000000000000 ) ) ;
#8163=LINE ( 'NONE', #6297, #7833 ) ;
#8164=ORIENTED_EDGE ( 'NONE', *, *, #10057, .T. ) ;
#8224=LINE ( 'NONE', #22851, #5056 ) ;
#8229=FACE_OUTER_BOUND ( 'NONE', #4682, .T. ) ;
#8232=CARTESIAN_POINT ( 'NONE',  ( -5.588000000000000078, -3660.140000000000327, 2250.998800000000301 ) ) ;
#8254=CARTESIAN_POINT ( 'NONE',  ( -0.7620000000000000107, -3578.860000000000127, 2247.392000000000280 ) ) ;
#8258=CARTESIAN_POINT ( 'NONE',  ( 3.048000000000000043, -3694.938000000000102, 2228.849999999999909 ) ) ;
#8262=LINE ( 'NONE', #15067, #9465 ) ;
#8293=VECTOR ( 'NONE', #1347, 1000.000000000000000 ) ;
#8297=ORIENTED_EDGE ( 'NONE', *, *, #14853, .T. ) ;
#8323=DIRECTION ( 'NONE',  ( -1.000000000000000000, 0.000000000000000000, 0.000000000000000000 ) ) ;
#8369=VERTEX_POINT ( 'NONE', #6486 ) ;
#8378=LINE ( 'NONE', #4854, #8480 ) ;
#8397=DIRECTION ( 'NONE',  ( 0.000000000000000000, -1.000000000000000000, 0.000000000000000000 ) ) ;
#8412=DIRECTION ( 'NONE',  ( 1.000000000000000000, 0.000000000000000000, 0.000000000000000000 ) ) ;
#8417=FACE_OUTER_BOUND ( 'NONE', #22704, .T. ) ;
#8418=ADVANCED_FACE ( 'NONE', ( #13396 ), #18551, .T. ) ;
#8427=AXIS2_PLACEMENT_3D ( 'NONE', #19619, #21379, #9073 ) ;
#8430=ORIENTED_EDGE ( 'NONE', *, *, #22743, .F. ) ;
#8431=FACE_OUTER_BOUND ( 'NONE', #6347, .T. ) ;
#8435=DIRECTION ( 'NONE',  ( 1.000000000000000000, 0.000000000000000000, 0.000000000000000000 ) ) ;
#8444=ORIENTED_EDGE ( 'NONE', *, *, #691, .F. ) ;
#8445=PRODUCT_DEFINITION_SHAPE ( 'NONE', 'NONE',  #1759 ) ;
#8450=CARTESIAN_POINT ( 'NONE',  ( -0.7620000000000000107, -3694.938000000000102, 2254.250000000000000 ) ) ;
#8463=DIRECTION ( 'NONE',  ( 0.000000000000000000, 0.000000000000000000, -1.000000000000000000 ) ) ;
#8475=AXIS2_PLACEMENT_3D ( 'NONE', #17036, #6283, #15065 ) ;
#8480=VECTOR ( 'NONE', #22659, 1000.000000000000000 ) ;
#8488=FACE_OUTER_BOUND ( 'NONE', #1886, .T. ) ;
#8494=ORIENTED_EDGE ( 'NONE', *, *, #14031, .F. ) ;
#8499=VERTEX_POINT ( 'NONE', #14096 ) ;
#8501=DIRECTION ( 'NONE',  ( 0.000000000000000000, 0.000000000000000000, -1.000000000000000000 ) ) ;
#8510=DIRECTION ( 'NONE',  ( -1.000000000000000000, 0.000000000000000000, 0.000000000000000000 ) ) ;
#8524=EDGE_CURVE ( 'NONE', #9973, #20183, #13729, .T. ) ;
#8527=LINE ( 'NONE', #22688, #6542 ) ;
#8551=ADVANCED_FACE ( 'NONE', ( #8587 ), #1309, .F. ) ;
#8584=DIRECTION ( 'NONE',  ( 0.000000000000000000, 0.000000000000000000, 1.000000000000000000 ) ) ;
#8587=FACE_OUTER_BOUND ( 'NONE', #56, .T. ) ;
#8619=CARTESIAN_POINT ( 'NONE',  ( -5.588000000000000078, -3694.938000000000102, 2254.250000000000000 ) ) ;
#8634=LINE ( 'NONE', #6771, #13686 ) ;
#8666=ORIENTED_EDGE ( 'NONE', *, *, #6930, .F. ) ;
#8681=FACE_OUTER_BOUND ( 'NONE', #12388, .T. ) ;
#8684=ORIENTED_EDGE ( 'NONE', *, *, #20102, .F. ) ;
#8700=DIRECTION ( 'NONE',  ( 0.000000000000000000, 0.000000000000000000, 1.000000000000000000 ) ) ;
#8701=DIRECTION ( 'NONE',  ( 0.000000000000000000, 0.000000000000000000, 1.000000000000000000 ) ) ;
#8723=ORIENTED_EDGE ( 'NONE', *, *, #6930, .T. ) ;
#8736=DIRECTION ( 'NONE',  ( -1.000000000000000000, 0.000000000000000000, 0.000000000000000000 ) ) ;
#8765=CARTESIAN_POINT ( 'NONE',  ( -6.349999999999999645, -3694.938000000000102, 2253.487999999999829 ) ) ;
#8834=CARTESIAN_POINT ( 'NONE',  ( 0.000000000000000000, -3660.140000000000327, 2247.392000000000280 ) ) ;
#8861=ADVANCED_FACE ( 'NONE', ( #936 ), #11879, .T. ) ;
#8881=ORIENTED_EDGE ( 'NONE', *, *, #145, .T. ) ;
#8944=VERTEX_POINT ( 'NONE', #22728 ) ;
#8957=FACE_OUTER_BOUND ( 'NONE', #1806, .T. ) ;
#8964=CIRCLE ( 'NONE', #5598, 0.7619999999999294005 ) ;
#8978=DIRECTION ( 'NONE',  ( -1.000000000000000000, 0.000000000000000000, 0.000000000000000000 ) ) ;
#8980=ORIENTED_EDGE ( 'NONE', *, *, #10431, .T. ) ;
#8986=ORIENTED_EDGE ( 'NONE', *, *, #10558, .F. ) ;
#9011=DIRECTION ( 'NONE',  ( -1.000000000000000000, 0.000000000000000000, 0.000000000000000000 ) ) ;
#9019=ADVANCED_FACE ( 'NONE', ( #9141 ), #18040, .T. ) ;
#9031=ORIENTED_EDGE ( 'NONE', *, *, #18248, .T. ) ;
#9067=ORIENTED_EDGE ( 'NONE', *, *, #13323, .F. ) ;
#9073=DIRECTION ( 'NONE',  ( 0.000000000000000000, 0.000000000000000000, 1.000000000000000000 ) ) ;
#9089=DIRECTION ( 'NONE',  ( 0.000000000000000000, 0.000000000000000000, -1.000000000000000000 ) ) ;
#9120=DIRECTION ( 'NONE',  ( -1.000000000000000000, 0.000000000000000000, 0.000000000000000000 ) ) ;
#9124=EDGE_LOOP ( 'NONE', ( #14182, #19654, #19039, #15489 ) ) ;
#9132=ADVANCED_FACE ( 'NONE', ( #1990 ), #19758, .T. ) ;
#9141=FACE_OUTER_BOUND ( 'NONE', #6519, .T. ) ;
#9184=EDGE_LOOP ( 'NONE', ( #19283, #9031, #10177, #13830 ) ) ;
#9187=ORIENTED_EDGE ( 'NONE', *, *, #23021, .F. ) ;
#9190=DIRECTION ( 'NONE',  ( 1.000000000000000000, 0.000000000000000000, 0.000000000000000000 ) ) ;
#9270=CARTESIAN_POINT ( 'NONE',  ( -6.349999999999999645, -3660.140000000000327, 2250.998800000000301 ) ) ;
#9287=EDGE_LOOP ( 'NONE', ( #4423, #5335, #9667, #5666 ) ) ;
#9294=ORIENTED_EDGE ( 'NONE', *, *, #12583, .T. ) ;
#9321=CARTESIAN_POINT ( 'NONE',  ( 0.7620000000000000107, -3544.061999999999898, 2239.009999999999764 ) ) ;
#9329=FACE_OUTER_BOUND ( 'NONE', #7299, .T. ) ;
#9378=EDGE_CURVE ( 'NONE', #22614, #11141, #11900, .T. ) ;
#9418=CARTESIAN_POINT ( 'NONE',  ( -5.588000000000000078, -3694.938000000000102, 2229.612000000000080 ) ) ;
#9435=AXIS2_PLACEMENT_3D ( 'NONE', #19020, #17252, #17136 ) ;
#9465=VECTOR ( 'NONE', #22198, 1000.000000000000000 ) ;
#9499=SHAPE_REPRESENTATION ( 'Support Ledge', ( #5611 ), #4481 ) ;
#9541=CARTESIAN_POINT ( 'NONE',  ( -0.7620000000000000107, -3544.061999999999898, 2228.849999999999909 ) ) ;
#9568=VECTOR ( 'NONE', #314, 1000.000000000000000 ) ;
#9580=DIRECTION ( 'NONE',  ( 0.000000000000000000, -1.000000000000000000, 0.000000000000000000 ) ) ;
#9591=CIRCLE ( 'NONE', #17764, 3.606800000000021100 ) ;
#9593=AXIS2_PLACEMENT_3D ( 'NONE', #14999, #22132, #6102 ) ;
#9595=ORIENTED_EDGE ( 'NONE', *, *, #1701, .T. ) ;
#9597=AXIS2_PLACEMENT_3D ( 'NONE', #9541, #12719, #2290 ) ;
#9617=ORIENTED_EDGE ( 'NONE', *, *, #10353, .F. ) ;
#9626=DIRECTION ( 'NONE',  ( 0.000000000000000000, 1.000000000000000000, 0.000000000000000000 ) ) ;
#9628=FACE_OUTER_BOUND ( 'NONE', #3440, .T. ) ;
#9637=AXIS2_PLACEMENT_3D ( 'NONE', #1604, #5140, #3479 ) ;
#9656=VECTOR ( 'NONE', #13038, 1000.000000000000000 ) ;
#9665=DIRECTION ( 'NONE',  ( -1.000000000000000000, 0.000000000000000000, 0.000000000000000000 ) ) ;
#9667=ORIENTED_EDGE ( 'NONE', *, *, #12583, .F. ) ;
#9677=ORIENTED_EDGE ( 'NONE', *, *, #22299, .F. ) ;
#9687=ORIENTED_EDGE ( 'NONE', *, *, #16004, .F. ) ;
#9726=CARTESIAN_POINT ( 'NONE',  ( -5.588000000000000078, -3694.938000000000102, 2228.849999999999909 ) ) ;
#9738=DIRECTION ( 'NONE',  ( 1.000000000000000000, 0.000000000000000000, 0.000000000000000000 ) ) ;
#9742=ORIENTED_EDGE ( 'NONE', *, *, #22718, .F. ) ;
#9743=CARTESIAN_POINT ( 'NONE',  ( -0.7620000000000000107, -3695.699999999999818, 2253.487999999999829 ) ) ;
#9751=DIRECTION ( 'NONE',  ( 0.000000000000000000, 0.000000000000000000, 1.000000000000000000 ) ) ;
#9759=LINE ( 'NONE', #11186, #21440 ) ;
#9768=EDGE_CURVE ( 'NONE', #7518, #5042, #21932, .T. ) ;
#9776=DIRECTION ( 'NONE',  ( 0.000000000000000000, 0.000000000000000000, 1.000000000000000000 ) ) ;
#9811=ADVANCED_FACE ( 'NONE', ( #8108 ), #315, .T. ) ;
#9849=EDGE_CURVE ( 'NONE', #21067, #20079, #14112, .T. ) ;
#9859=EDGE_CURVE ( 'NONE', #18858, #14398, #16399, .T. ) ;
#9878=VECTOR ( 'NONE', #15901, 1000.000000000000000 ) ;
#9888=DIRECTION ( 'NONE',  ( 1.000000000000000000, 0.000000000000000000, 0.000000000000000000 ) ) ;
#9902=CIRCLE ( 'NONE', #4318, 0.7619999999999996776 ) ;
#9921=ADVANCED_FACE ( 'NONE', ( #9628 ), #16772, .T. ) ;
#9954=CARTESIAN_POINT ( 'NONE',  ( -0.7620000000000000107, -3544.061999999999898, 2239.771999999999935 ) ) ;
#9973=VERTEX_POINT ( 'NONE', #3627 ) ;
#10014=VERTEX_POINT ( 'NONE', #16287 ) ;
#10017=CARTESIAN_POINT ( 'NONE',  ( -6.349999999999999645, -3660.140000000000327, 2247.392000000000280 ) ) ;
#10032=ORIENTED_EDGE ( 'NONE', *, *, #18982, .T. ) ;
#10057=EDGE_CURVE ( 'NONE', #5906, #9973, #14868, .T. ) ;
#10062=SPHERICAL_SURFACE ( 'NONE', #22948, 0.7620000000000000107 ) ;
#10070=EDGE_CURVE ( 'NONE', #15388, #7817, #7016, .T. ) ;
#10077=AXIS2_PLACEMENT_3D ( 'NONE', #23019, #3228, #14249 ) ;
#10086=ORIENTED_EDGE ( 'NONE', *, *, #17971, .F. ) ;
#10100=PRODUCT_DEFINITION_FORMATION_WITH_SPECIFIED_SOURCE ( 'ANY', '', #11987, .NOT_KNOWN. ) ;
#10120=EDGE_LOOP ( 'NONE', ( #8684, #2589, #14124, #14665, #8494, #8444, #8986 ) ) ;
#10129=DIRECTION ( 'NONE',  ( 1.000000000000000000, 0.000000000000000000, 0.000000000000000000 ) ) ;
#10140=FACE_BOUND ( 'NONE', #6988, .T. ) ;
#10142=VECTOR ( 'NONE', #2423, 1000.000000000000000 ) ;
#10144=CARTESIAN_POINT ( 'NONE',  ( -0.7620000000000000107, -3578.860000000000127, 2247.392000000000280 ) ) ;
#10167=DIRECTION ( 'NONE',  ( 0.000000000000000000, 0.000000000000000000, -1.000000000000000000 ) ) ;
#10172=EDGE_LOOP ( 'NONE', ( #17107, #6074, #5151, #18176 ) ) ;
#10177=ORIENTED_EDGE ( 'NONE', *, *, #7583, .T. ) ;
#10179=DIRECTION ( 'NONE',  ( 0.000000000000000000, 1.000000000000000000, 0.000000000000000000 ) ) ;
#10206=DIRECTION ( 'NONE',  ( 0.000000000000000000, -1.000000000000000000, 0.000000000000000000 ) ) ;
#10284=CARTESIAN_POINT ( 'NONE',  ( 3.048000000000000043, -3544.061999999999898, 2229.612000000000080 ) ) ;
#10292=AXIS2_PLACEMENT_3D ( 'NONE', #17124, #13617, #4822 ) ;
#10321=VECTOR ( 'NONE', #11663, 1000.000000000000000 ) ;
#10330=ORIENTED_EDGE ( 'NONE', *, *, #21718, .F. ) ;
#10351=AXIS2_PLACEMENT_3D ( 'NONE', #4378, #18662, #2840 ) ;
#10353=EDGE_CURVE ( 'NONE', #5628, #3849, #15566, .T. ) ;
#10355=ORIENTED_EDGE ( 'NONE', *, *, #17971, .T. ) ;
#10359=AXIS2_PLACEMENT_3D ( 'NONE', #21139, #12229, #17608 ) ;
#10387=DIRECTION ( 'NONE',  ( 0.000000000000000000, -1.000000000000000000, 0.000000000000000000 ) ) ;
#10388=EDGE_CURVE ( 'NONE', #16359, #20183, #16150, .T. ) ;
#10395=ORIENTED_EDGE ( 'NONE', *, *, #7941, .F. ) ;
#10397=AXIS2_PLACEMENT_3D ( 'NONE', #2851, #13630, #20777 ) ;
#10405=DIRECTION ( 'NONE',  ( 1.000000000000000000, 0.000000000000000000, 0.000000000000000000 ) ) ;
#10426=AXIS2_PLACEMENT_3D ( 'NONE', #22220, #2328, #7715 ) ;
#10431=EDGE_CURVE ( 'NONE', #18259, #8944, #3972, .T. ) ;
#10454=CARTESIAN_POINT ( 'NONE',  ( -0.7620000000000000107, -3544.061999999999898, 2253.487999999999829 ) ) ;
#10480=FACE_OUTER_BOUND ( 'NONE', #6037, .T. ) ;
#10512=ORIENTED_EDGE ( 'NONE', *, *, #22697, .F. ) ;
#10540=ORIENTED_EDGE ( 'NONE', *, *, #10986, .F. ) ;
#10544=CYLINDRICAL_SURFACE ( 'NONE', #10989, 0.7620000000000000107 ) ;
#10558=EDGE_CURVE ( 'NONE', #18858, #20500, #8378, .T. ) ;
#10651=EDGE_CURVE ( 'NONE', #20183, #8499, #19974, .T. ) ;
#10685=DIRECTION ( 'NONE',  ( 1.000000000000000000, 0.000000000000000000, 0.000000000000000000 ) ) ;
#10728=DIRECTION ( 'NONE',  ( 1.000000000000000000, 0.000000000000000000, 0.000000000000000000 ) ) ;
#10730=EDGE_LOOP ( 'NONE', ( #12566, #11853, #17024 ) ) ;
#10737=EDGE_CURVE ( 'NONE', #5364, #12671, #16445, .T. ) ;
#10749=AXIS2_PLACEMENT_3D ( 'NONE', #12542, #18155, #17921 ) ;
#10798=ORIENTED_EDGE ( 'NONE', *, *, #220, .T. ) ;
#10863=CARTESIAN_POINT ( 'NONE',  ( 0.7620000000000000107, -3544.061999999999898, 2239.009999999999764 ) ) ;
#10870=AXIS2_PLACEMENT_3D ( 'NONE', #5652, #14670, #7290 ) ;
#10871=DIRECTION ( 'NONE',  ( 0.000000000000000000, 1.000000000000000000, 0.000000000000000000 ) ) ;
#10937=EDGE_LOOP ( 'NONE', ( #3619, #11383, #4799 ) ) ;
#10954=AXIS2_PLACEMENT_3D ( 'NONE', #12359, #17272, #19159 ) ;
#10955=AXIS2_PLACEMENT_3D ( 'NONE', #4651, #22692, #22917 ) ;
#10959=DIRECTION ( 'NONE',  ( 0.000000000000000000, -1.000000000000000000, 0.000000000000000000 ) ) ;
#10965=ORIENTED_EDGE ( 'NONE', *, *, #17064, .T. ) ;
#10986=EDGE_CURVE ( 'NONE', #5628, #2574, #19705, .T. ) ;
#10989=AXIS2_PLACEMENT_3D ( 'NONE', #8450, #14066, #15706 ) ;
#10991=VECTOR ( 'NONE', #10206, 1000.000000000000000 ) ;
#11006=CARTESIAN_POINT ( 'NONE',  ( 0.7620000000000000107, -3544.061999999999898, 2239.771999999999935 ) ) ;
#11031=DIRECTION ( 'NONE',  ( 0.000000000000000000, 0.000000000000000000, 1.000000000000000000 ) ) ;
#11032=CARTESIAN_POINT ( 'NONE',  ( -5.588000000000000078, -3578.860000000000127, 2247.392000000000280 ) ) ;
#11059=AXIS2_PLACEMENT_3D ( 'NONE', #5007, #21298, #5240 ) ;
#11084=ADVANCED_FACE ( 'NONE', ( #8431 ), #1498, .F. ) ;
#11088=ORIENTED_EDGE ( 'NONE', *, *, #15136, .F. ) ;
#11114=ADVANCED_FACE ( 'NONE', ( #15578, #14177, #6792 ), #21320, .F. ) ;
#11117=LINE ( 'NONE', #20245, #2108 ) ;
#11141=VERTEX_POINT ( 'NONE', #12175 ) ;
#11158=PRODUCT_CONTEXT ( 'NONE', #16793, 'mechanical' ) ;
#11161=CARTESIAN_POINT ( 'NONE',  ( 0.000000000000000000, -3694.938000000000102, 2253.487999999999829 ) ) ;
#11186=CARTESIAN_POINT ( 'NONE',  ( -5.588000000000000078, -3694.938000000000102, 2254.250000000000000 ) ) ;
#11249=AXIS2_PLACEMENT_3D ( 'NONE', #8232, #3068, #8701 ) ;
#11255=DIRECTION ( 'NONE',  ( 0.000000000000000000, 0.000000000000000000, 1.000000000000000000 ) ) ;
#11301=CARTESIAN_POINT ( 'NONE',  ( -0.7620000000000000107, -3660.140000000000327, 2244.547199999999975 ) ) ;
#11308=VECTOR ( 'NONE', #5371, 1000.000000000000000 ) ;
#11311=CARTESIAN_POINT ( 'NONE',  ( -0.7620000000000000107, -3660.140000000000327, 2250.236800000000130 ) ) ;
#11313=AXIS2_PLACEMENT_3D ( 'NONE', #15912, #11802, #8412 ) ;
#11383=ORIENTED_EDGE ( 'NONE', *, *, #4975, .T. ) ;
#11403=AXIS2_PLACEMENT_3D ( 'NONE', #4814, #7904, #8463 ) ;
#11493=FACE_OUTER_BOUND ( 'NONE', #20314, .T. ) ;
#11531=EDGE_LOOP ( 'NONE', ( #2661, #4668, #14350, #14908 ) ) ;
#11535=DIRECTION ( 'NONE',  ( 1.000000000000000000, 0.000000000000000000, 0.000000000000000000 ) ) ;
#11564=ADVANCED_FACE ( 'NONE', ( #9329 ), #7226, .F. ) ;
#11572=DIRECTION ( 'NONE',  ( 0.000000000000000000, 1.000000000000000000, 0.000000000000000000 ) ) ;
#11596=DIRECTION ( 'NONE',  ( 0.000000000000000000, 0.000000000000000000, 1.000000000000000000 ) ) ;
#11605=LINE ( 'NONE', #6358, #1723 ) ;
#11607=ORIENTED_EDGE ( 'NONE', *, *, #17983, .T. ) ;
#11641=EDGE_CURVE ( 'NONE', #3849, #20079, #6155, .T. ) ;
#11663=DIRECTION ( 'NONE',  ( -1.000000000000000000, 0.000000000000000000, 0.000000000000000000 ) ) ;
#11723=AXIS2_PLACEMENT_3D ( 'NONE', #22086, #14957, #8154 ) ;
#11732=CARTESIAN_POINT ( 'NONE',  ( -5.588000000000000078, -3544.061999999999898, 2229.612000000000080 ) ) ;
#11737=VERTEX_POINT ( 'NONE', #13764 ) ;
#11748=FACE_OUTER_BOUND ( 'NONE', #10172, .T. ) ;
#11750=LINE ( 'NONE', #739, #12616 ) ;
#11753=EDGE_LOOP ( 'NONE', ( #921, #6499, #22258, #8430, #18255, #7014, #17325 ) ) ;
#11767=ORIENTED_EDGE ( 'NONE', *, *, #1701, .F. ) ;
#11774=CARTESIAN_POINT ( 'NONE',  ( -0.7620000000000000107, -3694.938000000000102, 2254.250000000000000 ) ) ;
#11800=ORIENTED_EDGE ( 'NONE', *, *, #3541, .F. ) ;
#11802=DIRECTION ( 'NONE',  ( 0.000000000000000000, 0.000000000000000000, 1.000000000000000000 ) ) ;
#11810=AXIS2_PLACEMENT_3D ( 'NONE', #1745, #15805, #22711 ) ;
#11852=AXIS2_PLACEMENT_3D ( 'NONE', #5820, #3809, #13067 ) ;
#11853=ORIENTED_EDGE ( 'NONE', *, *, #9859, .T. ) ;
#11860=CARTESIAN_POINT ( 'NONE',  ( -5.588000000000000078, -3544.061999999999898, 2229.612000000000080 ) ) ;
#11879=TOROIDAL_SURFACE ( 'NONE', #21983, 1.524000000000000021, 0.7620000000000000107 ) ;
#11884=DIRECTION ( 'NONE',  ( 0.000000000000000000, 0.000000000000000000, -1.000000000000000000 ) ) ;
#11894=DIRECTION ( 'NONE',  ( -1.000000000000000000, 0.000000000000000000, 0.000000000000000000 ) ) ;
#11900=CIRCLE ( 'NONE', #9637, 0.7619999999999996776 ) ;
#11922=ORIENTED_EDGE ( 'NONE', *, *, #1493, .F. ) ;
#11952=FACE_OUTER_BOUND ( 'NONE', #21341, .T. ) ;
#11963=CIRCLE ( 'NONE', #19445, 2.844800000000091700 ) ;
#11987=PRODUCT ( 'Support Ledge', 'Support Ledge', '', ( #11158 ) ) ;
#11996=AXIS2_PLACEMENT_3D ( 'NONE', #20617, #16138, #17650 ) ;
#12022=ORIENTED_EDGE ( 'NONE', *, *, #628, .T. ) ;
#12033=DIRECTION ( 'NONE',  ( 1.000000000000000000, 0.000000000000000000, 0.000000000000000000 ) ) ;
#12042=ORIENTED_EDGE ( 'NONE', *, *, #14820, .T. ) ;
#12049=CIRCLE ( 'NONE', #3876, 1.523999999999858801 ) ;
#12079=DIRECTION ( 'NONE',  ( 0.000000000000000000, 0.000000000000000000, 1.000000000000000000 ) ) ;
#12109=EDGE_CURVE ( 'NONE', #5628, #21067, #7140, .T. ) ;
#12132=CARTESIAN_POINT ( 'NONE',  ( 0.7620000000000000107, -3543.299999999999727, 2238.248000000000047 ) ) ;
#12135=VERTEX_POINT ( 'NONE', #3495 ) ;
#12150=CARTESIAN_POINT ( 'NONE',  ( -6.349999999999999645, -3660.140000000000327, 2243.785200000000259 ) ) ;
#12157=FACE_OUTER_BOUND ( 'NONE', #9287, .T. ) ;
#12175=CARTESIAN_POINT ( 'NONE',  ( -5.588000000000000078, -3694.938000000000102, 2228.849999999999909 ) ) ;
#12195=AXIS2_PLACEMENT_3D ( 'NONE', #6421, #16833, #20361 ) ;
#12229=DIRECTION ( 'NONE',  ( 0.000000000000000000, 0.000000000000000000, 1.000000000000000000 ) ) ;
#12230=ORIENTED_EDGE ( 'NONE', *, *, #20896, .F. ) ;
#12233=AXIS2_PLACEMENT_3D ( 'NONE', #17112, #4578, #4241 ) ;
#12243=ORIENTED_EDGE ( 'NONE', *, *, #22253, .T. ) ;
#12248=FACE_OUTER_BOUND ( 'NONE', #11531, .T. ) ;
#12255=LINE ( 'NONE', #15769, #8293 ) ;
#12290=LINE ( 'NONE', #21316, #21476 ) ;
#12302=CARTESIAN_POINT ( 'NONE',  ( 3.810000000000000053, -3695.699999999999818, 2228.849999999999909 ) ) ;
#12315=CARTESIAN_POINT ( 'NONE',  ( 3.048000000000000043, -3544.061999999999898, 2229.612000000000080 ) ) ;
#12324=ADVANCED_FACE ( 'NONE', ( #12990 ), #12755, .F. ) ;
#12331=DIRECTION ( 'NONE',  ( -1.000000000000000000, 0.000000000000000000, 0.000000000000000000 ) ) ;
#12359=CARTESIAN_POINT ( 'NONE',  ( 0.000000000000000000, -3543.299999999999727, 2239.009999999999764 ) ) ;
#12361=ORIENTED_EDGE ( 'NONE', *, *, #21485, .T. ) ;
#12367=DIRECTION ( 'NONE',  ( 0.000000000000000000, 0.000000000000000000, 1.000000000000000000 ) ) ;
#12381=DIRECTION ( 'NONE',  ( 0.000000000000000000, 1.000000000000000000, 0.000000000000000000 ) ) ;
#12388=EDGE_LOOP ( 'NONE', ( #10798, #1646, #19641, #17561 ) ) ;
#12397=DIRECTION ( 'NONE',  ( 0.000000000000000000, 0.000000000000000000, 1.000000000000000000 ) ) ;
#12423=CARTESIAN_POINT ( 'NONE',  ( -6.349999999999999645, -3578.860000000000127, 2247.392000000000280 ) ) ;
#12429=FACE_OUTER_BOUND ( 'NONE', #15948, .T. ) ;
#12460=CIRCLE ( 'NONE', #835, 3.606800000000021100 ) ;
#12476=FACE_OUTER_BOUND ( 'NONE', #18139, .T. ) ;
#12534=CARTESIAN_POINT ( 'NONE',  ( 3.048000000000000043, -3694.938000000000102, 2229.612000000000080 ) ) ;
#12542=CARTESIAN_POINT ( 'NONE',  ( -0.7620000000000000107, -3544.061999999999898, 2253.487999999999829 ) ) ;
#12543=DIRECTION ( 'NONE',  ( 1.000000000000000000, 0.000000000000000000, 0.000000000000000000 ) ) ;
#12566=ORIENTED_EDGE ( 'NONE', *, *, #5088, .T. ) ;
#12583=EDGE_CURVE ( 'NONE', #8369, #11141, #8527, .T. ) ;
#12597=EDGE_CURVE ( 'NONE', #13004, #1122, #22911, .T. ) ;
#12616=VECTOR ( 'NONE', #22407, 1000.000000000000000 ) ;
#12654=AXIS2_PLACEMENT_3D ( 'NONE', #718, #16992, #15024 ) ;
#12671=VERTEX_POINT ( 'NONE', #21183 ) ;
#12676=DIRECTION ( 'NONE',  ( 0.000000000000000000, 0.000000000000000000, 1.000000000000000000 ) ) ;
#12679=DIRECTION ( 'NONE',  ( 0.000000000000000000, 0.000000000000000000, 1.000000000000000000 ) ) ;
#12707=ADVANCED_FACE ( 'NONE', ( #7114 ), #5238, .T. ) ;
#12709=CARTESIAN_POINT ( 'NONE',  ( -5.588000000000000078, -3660.140000000000327, 2247.392000000000280 ) ) ;
#12719=DIRECTION ( 'NONE',  ( 0.000000000000000000, 0.000000000000000000, 1.000000000000000000 ) ) ;
#12755=CYLINDRICAL_SURFACE ( 'NONE', #578, 2.844800000000091700 ) ;
#12790=DIRECTION ( 'NONE',  ( 0.000000000000000000, -1.000000000000000000, 0.000000000000000000 ) ) ;
#12820=CARTESIAN_POINT ( 'NONE',  ( -5.588000000000000078, -3544.061999999999898, 2254.250000000000000 ) ) ;
#12831=DIRECTION ( 'NONE',  ( 0.000000000000000000, 0.000000000000000000, -1.000000000000000000 ) ) ;
#12902=AXIS2_PLACEMENT_3D ( 'NONE', #15427, #19057, #8397 ) ;
#12924=ORIENTED_EDGE ( 'NONE', *, *, #9378, .T. ) ;
#12940=DIRECTION ( 'NONE',  ( -1.000000000000000000, 0.000000000000000000, 0.000000000000000000 ) ) ;
#12946=EDGE_LOOP ( 'NONE', ( #22021, #16382, #20080, #15193 ) ) ;
#12961=AXIS2_PLACEMENT_3D ( 'NONE', #10144, #15538, #4519 ) ;
#12990=FACE_OUTER_BOUND ( 'NONE', #12946, .T. ) ;
#12996=CARTESIAN_POINT ( 'NONE',  ( 3.810000000000000053, -3544.061999999999898, 2229.612000000000080 ) ) ;
#13004=VERTEX_POINT ( 'NONE', #8258 ) ;
#13038=DIRECTION ( 'NONE',  ( -1.000000000000000000, 0.000000000000000000, 0.000000000000000000 ) ) ;
#13061=DIRECTION ( 'NONE',  ( 0.000000000000000000, 1.000000000000000000, 0.000000000000000000 ) ) ;
#13067=DIRECTION ( 'NONE',  ( 0.000000000000000000, -1.000000000000000000, 0.000000000000000000 ) ) ;
#13073=DIRECTION ( 'NONE',  ( 0.000000000000000000, -1.000000000000000000, 0.000000000000000000 ) ) ;
#13107=EDGE_LOOP ( 'NONE', ( #15803, #5948, #346, #16823 ) ) ;
#13120=ORIENTED_EDGE ( 'NONE', *, *, #628, .F. ) ;
#13168=CARTESIAN_POINT ( 'NONE',  ( -0.7620000000000000107, -3543.299999999999727, 2253.487999999999829 ) ) ;
#13195=TOROIDAL_SURFACE ( 'NONE', #22907, 3.606799999999999784, 0.7620000000000000107 ) ;
#13210=DIRECTION ( 'NONE',  ( 1.000000000000000000, 0.000000000000000000, 0.000000000000000000 ) ) ;
#13238=ADVANCED_FACE ( 'NONE', ( #8957 ), #1808, .T. ) ;
#13281=AXIS2_PLACEMENT_3D ( 'NONE', #11860, #1304, #20888 ) ;
#13283=ORIENTED_EDGE ( 'NONE', *, *, #10986, .T. ) ;
#13298=DIRECTION ( 'NONE',  ( -1.000000000000000000, 0.000000000000000000, 0.000000000000000000 ) ) ;
#13318=AXIS2_PLACEMENT_3D ( 'NONE', #14125, #21034, #5102 ) ;
#13322=CARTESIAN_POINT ( 'NONE',  ( -5.588000000000000078, -3694.938000000000102, 2229.612000000000080 ) ) ;
#13323=EDGE_CURVE ( 'NONE', #7817, #15388, #14033, .T. ) ;
#13325=CARTESIAN_POINT ( 'NONE',  ( 0.7620000000000000107, -3543.299999999999727, 2239.771999999999935 ) ) ;
#13361=CYLINDRICAL_SURFACE ( 'NONE', #7194, 0.7619999999999996776 ) ;
#13396=FACE_OUTER_BOUND ( 'NONE', #22261, .T. ) ;
#13445=ORIENTED_EDGE ( 'NONE', *, *, #15739, .T. ) ;
#13447=LINE ( 'NONE', #2557, #16907 ) ;
#13449=VECTOR ( 'NONE', #22057, 1000.000000000000000 ) ;
#13488=ORIENTED_EDGE ( 'NONE', *, *, #20706, .T. ) ;
#13500=CARTESIAN_POINT ( 'NONE',  ( -0.7620000000000000107, -3694.938000000000102, 2253.487999999999829 ) ) ;
#13504=EDGE_CURVE ( 'NONE', #15888, #14896, #933, .T. ) ;
#13537=ADVANCED_FACE ( 'NONE', ( #8229 ), #22627, .T. ) ;
#13605=FACE_OUTER_BOUND ( 'NONE', #10120, .T. ) ;
#13616=CARTESIAN_POINT ( 'NONE',  ( 0.7620000000000000107, -3694.938000000000102, 2239.771999999999935 ) ) ;
#13617=DIRECTION ( 'NONE',  ( 0.000000000000000000, 0.000000000000000000, -1.000000000000000000 ) ) ;
#13621=( LENGTH_UNIT ( ) NAMED_UNIT ( * ) SI_UNIT ( .MILLI., .METRE. ) );
#13630=DIRECTION ( 'NONE',  ( 0.000000000000000000, 1.000000000000000000, 0.000000000000000000 ) ) ;
#13637=ORIENTED_EDGE ( 'NONE', *, *, #21485, .F. ) ;
#13686=VECTOR ( 'NONE', #1595, 1000.000000000000000 ) ;
#13708=AXIS2_PLACEMENT_3D ( 'NONE', #8254, #9665, #15403 ) ;
#13729=CIRCLE ( 'NONE', #4011, 0.7619999999999294005 ) ;
#13734=ORIENTED_EDGE ( 'NONE', *, *, #21910, .F. ) ;
#13737=CARTESIAN_POINT ( 'NONE',  ( -0.7620000000000000107, -3543.299999999999727, 2239.771999999999935 ) ) ;
#13764=CARTESIAN_POINT ( 'NONE',  ( -5.588000000000000078, -3660.140000000000327, 2250.236800000000130 ) ) ;
#13794=ORIENTED_EDGE ( 'NONE', *, *, #23162, .F. ) ;
#13812=DIRECTION ( 'NONE',  ( 0.000000000000000000, -1.000000000000000000, 0.000000000000000000 ) ) ;
#13830=ORIENTED_EDGE ( 'NONE', *, *, #20706, .F. ) ;
#13835=ADVANCED_FACE ( 'NONE', ( #17182 ), #4111, .F. ) ;
#13838=DIRECTION ( 'NONE',  ( -0.000000000000000000, 1.000000000000000000, 0.000000000000000000 ) ) ;
#13855=FACE_OUTER_BOUND ( 'NONE', #4007, .T. ) ;
#13961=CARTESIAN_POINT ( 'NONE',  ( 0.7620000000000000107, -3694.938000000000102, 2239.009999999999764 ) ) ;
#13972=DIRECTION ( 'NONE',  ( 0.000000000000000000, 0.000000000000000000, -1.000000000000000000 ) ) ;
#13994=CIRCLE ( 'NONE', #18832, 2.844800000000091700 ) ;
#14031=EDGE_CURVE ( 'NONE', #3687, #7518, #8262, .T. ) ;
#14033=CIRCLE ( 'NONE', #8427, 3.606800000000021100 ) ;
#14041=CYLINDRICAL_SURFACE ( 'NONE', #5340, 0.7620000000000001217 ) ;
#14048=VECTOR ( 'NONE', #20966, 1000.000000000000000 ) ;
#14052=ORIENTED_EDGE ( 'NONE', *, *, #7835, .F. ) ;
#14055=ORIENTED_EDGE ( 'NONE', *, *, #691, .T. ) ;
#14066=DIRECTION ( 'NONE',  ( 0.000000000000000000, 0.000000000000000000, -1.000000000000000000 ) ) ;
#14096=CARTESIAN_POINT ( 'NONE',  ( 0.000000000000000000, -3544.061999999999898, 2239.771999999999935 ) ) ;
#14098=EDGE_CURVE ( 'NONE', #7086, #22455, #12460, .T. ) ;
#14112=CIRCLE ( 'NONE', #15280, 2.844800000000091700 ) ;
#14124=ORIENTED_EDGE ( 'NONE', *, *, #20185, .T. ) ;
#14125=CARTESIAN_POINT ( 'NONE',  ( 3.048000000000000043, -3694.938000000000102, 2238.248000000000047 ) ) ;
#14128=CIRCLE ( 'NONE', #4018, 0.7619999999999294005 ) ;
#14138=ORIENTED_EDGE ( 'NONE', *, *, #16934, .F. ) ;
#14177=FACE_BOUND ( 'NONE', #4109, .T. ) ;
#14180=ADVANCED_FACE ( 'NONE', ( #12248 ), #6864, .F. ) ;
#14182=ORIENTED_EDGE ( 'NONE', *, *, #10651, .F. ) ;
#14205=ORIENTED_EDGE ( 'NONE', *, *, #5973, .F. ) ;
#14225=ORIENTED_EDGE ( 'NONE', *, *, #17064, .F. ) ;
#14237=EDGE_CURVE ( 'NONE', #18263, #1122, #22912, .T. ) ;
#14249=DIRECTION ( 'NONE',  ( 0.000000000000000000, 0.000000000000000000, 1.000000000000000000 ) ) ;
#14265=ADVANCED_FACE ( 'NONE', ( #12476 ), #2982, .T. ) ;
#14272=CARTESIAN_POINT ( 'NONE',  ( -6.349999999999999645, -3578.860000000000127, 2243.785200000000259 ) ) ;
#14282=ORIENTED_EDGE ( 'NONE', *, *, #14477, .T. ) ;
#14319=AXIS2_PLACEMENT_3D ( 'NONE', #19169, #8510, #6872 ) ;
#14330=DIRECTION ( 'NONE',  ( 1.000000000000000000, 0.000000000000000000, 0.000000000000000000 ) ) ;
#14345=ORIENTED_EDGE ( 'NONE', *, *, #220, .F. ) ;
#14350=ORIENTED_EDGE ( 'NONE', *, *, #6576, .F. ) ;
#14356=CARTESIAN_POINT ( 'NONE',  ( -5.588000000000000078, -3695.699999999999818, 2229.612000000000080 ) ) ;
#14395=EDGE_CURVE ( 'NONE', #15888, #16359, #19858, .T. ) ;
#14398=VERTEX_POINT ( 'NONE', #18094 ) ;
#14420=DIRECTION ( 'NONE',  ( 0.000000000000000000, 0.000000000000000000, 1.000000000000000000 ) ) ;
#14446=DIRECTION ( 'NONE',  ( 0.000000000000000000, 1.000000000000000000, 1.224646799147353207E-16 ) ) ;
#14455=CIRCLE ( 'NONE', #3209, 1.524000000000000021 ) ;
#14477=EDGE_CURVE ( 'NONE', #10014, #20881, #6492, .T. ) ;
#14530=DIRECTION ( 'NONE',  ( -3.130242492740591634E-14, 0.000000000000000000, -1.000000000000000000 ) ) ;
#14553=EDGE_LOOP ( 'NONE', ( #20860, #4365, #14942 ) ) ;
#14573=VECTOR ( 'NONE', #4401, 1000.000000000000000 ) ;
#14582=AXIS2_PLACEMENT_3D ( 'NONE', #3338, #17516, #3574 ) ;
#14598=ORIENTED_EDGE ( 'NONE', *, *, #7505, .F. ) ;
#14609=ORIENTED_EDGE ( 'NONE', *, *, #1960, .F. ) ;
#14665=ORIENTED_EDGE ( 'NONE', *, *, #9768, .F. ) ;
#14670=DIRECTION ( 'NONE',  ( 0.000000000000000000, -1.000000000000000000, 0.000000000000000000 ) ) ;
#14680=ORIENTED_EDGE ( 'NONE', *, *, #7583, .F. ) ;
#14692=VECTOR ( 'NONE', #16540, 1000.000000000000000 ) ;
#14700=LINE ( 'NONE', #12820, #13449 ) ;
#14708=TOROIDAL_SURFACE ( 'NONE', #482, 3.606799999999999784, 0.7620000000000000107 ) ;
#14728=VECTOR ( 'NONE', #1928, 1000.000000000000000 ) ;
#14747=ORIENTED_EDGE ( 'NONE', *, *, #7835, .T. ) ;
#14772=ORIENTED_EDGE ( 'NONE', *, *, #3541, .T. ) ;
#14773=DIRECTION ( 'NONE',  ( 1.000000000000000000, 0.000000000000000000, 0.000000000000000000 ) ) ;
#14785=DIRECTION ( 'NONE',  ( -1.000000000000000000, 0.000000000000000000, 0.000000000000000000 ) ) ;
#14812=EDGE_LOOP ( 'NONE', ( #16416, #19904, #9742, #23041 ) ) ;
#14820=EDGE_CURVE ( 'NONE', #19266, #4559, #4942, .T. ) ;
#14845=CIRCLE ( 'NONE', #4729, 0.7619999999999294005 ) ;
#14853=EDGE_CURVE ( 'NONE', #20079, #7817, #19979, .T. ) ;
#14857=VECTOR ( 'NONE', #1925, 1000.000000000000000 ) ;
#14868=CIRCLE ( 'NONE', #10749, 0.7619999999999294005 ) ;
#14896=VERTEX_POINT ( 'NONE', #6696 ) ;
#14899=ADVANCED_FACE ( 'NONE', ( #11952 ), #10544, .T. ) ;
#14908=ORIENTED_EDGE ( 'NONE', *, *, #16262, .F. ) ;
#14932=CYLINDRICAL_SURFACE ( 'NONE', #18767, 0.7619999999999294005 ) ;
#14942=ORIENTED_EDGE ( 'NONE', *, *, #5973, .T. ) ;
#14943=CARTESIAN_POINT ( 'NONE',  ( 1.270000000000000018, -3578.860000000000127, 2244.547199999999975 ) ) ;
#14957=DIRECTION ( 'NONE',  ( -1.000000000000000000, 0.000000000000000000, 0.000000000000000000 ) ) ;
#14999=CARTESIAN_POINT ( 'NONE',  ( -0.7620000000000000107, -3578.860000000000127, 2250.998800000000301 ) ) ;
#15005=EDGE_CURVE ( 'NONE', #767, #14896, #12049, .T. ) ;
#15011=DIRECTION ( 'NONE',  ( 1.000000000000000000, 0.000000000000000000, 0.000000000000000000 ) ) ;
#15024=DIRECTION ( 'NONE',  ( 0.000000000000000000, 0.000000000000000000, -1.000000000000000000 ) ) ;
#15046=DIRECTION ( 'NONE',  ( 0.000000000000000000, 0.000000000000000000, 1.000000000000000000 ) ) ;
#15065=DIRECTION ( 'NONE',  ( -1.000000000000000000, 0.000000000000000000, 0.000000000000000000 ) ) ;
#15067=CARTESIAN_POINT ( 'NONE',  ( 3.048000000000000043, -3543.299999999999727, 2229.612000000000080 ) ) ;
#15096=VECTOR ( 'NONE', #17812, 1000.000000000000000 ) ;
#15099=CIRCLE ( 'NONE', #4997, 0.7619999999999294005 ) ;
#15123=CARTESIAN_POINT ( 'NONE',  ( 0.7620000000000000107, -3544.061999999999898, 2238.248000000000047 ) ) ;
#15136=EDGE_CURVE ( 'NONE', #4281, #18259, #13447, .T. ) ;
#15174=LINE ( 'NONE', #2975, #22479 ) ;
#15182=AXIS2_PLACEMENT_3D ( 'NONE', #4792, #19868, #1388 ) ;
#15186=ORIENTED_EDGE ( 'NONE', *, *, #10070, .F. ) ;
#15193=ORIENTED_EDGE ( 'NONE', *, *, #20041, .F. ) ;
#15216=AXIS2_PLACEMENT_3D ( 'NONE', #12315, #18157, #5635 ) ;
#15267=CARTESIAN_POINT ( 'NONE',  ( 3.048000000000000043, -3544.061999999999898, 2228.849999999999909 ) ) ;
#15278=ADVANCED_FACE ( 'NONE', ( #12157 ), #1373, .F. ) ;
#15280=AXIS2_PLACEMENT_3D ( 'NONE', #1058, #6239, #6466 ) ;
#15285=VERTEX_POINT ( 'NONE', #8765 ) ;
#15294=CARTESIAN_POINT ( 'NONE',  ( 3.810000000000000053, -3694.938000000000102, 2229.612000000000080 ) ) ;
#15329=ORIENTED_EDGE ( 'NONE', *, *, #6427, .T. ) ;
#15348=VERTEX_POINT ( 'NONE', #10863 ) ;
#15388=VERTEX_POINT ( 'NONE', #207 ) ;
#15403=DIRECTION ( 'NONE',  ( 0.000000000000000000, 0.000000000000000000, 1.000000000000000000 ) ) ;
#15427=CARTESIAN_POINT ( 'NONE',  ( 3.048000000000000043, -3694.938000000000102, 2229.612000000000080 ) ) ;
#15489=ORIENTED_EDGE ( 'NONE', *, *, #17536, .F. ) ;
#15538=DIRECTION ( 'NONE',  ( -1.000000000000000000, 0.000000000000000000, 0.000000000000000000 ) ) ;
#15565=DIRECTION ( 'NONE',  ( -1.000000000000000000, 0.000000000000000000, 0.000000000000000000 ) ) ;
#15566=CIRCLE ( 'NONE', #18553, 2.844800000000091700 ) ;
#15578=FACE_BOUND ( 'NONE', #16457, .T. ) ;
#15586=VECTOR ( 'NONE', #19856, 1000.000000000000000 ) ;
#15590=EDGE_CURVE ( 'NONE', #19446, #15348, #2309, .T. ) ;
#15611=CARTESIAN_POINT ( 'NONE',  ( 3.048000000000000043, -3544.061999999999898, 2239.009999999999764 ) ) ;
#15622=( NAMED_UNIT ( * ) PLANE_ANGLE_UNIT ( ) SI_UNIT ( $, .RADIAN. ) );
#15627=AXIS2_PLACEMENT_3D ( 'NONE', #16877, #9626, #7871 ) ;
#15646=FACE_OUTER_BOUND ( 'NONE', #6693, .T. ) ;
#15650=VERTEX_POINT ( 'NONE', #8619 ) ;
#15663=CARTESIAN_POINT ( 'NONE',  ( -5.588000000000000078, -3543.299999999999727, 2253.487999999999829 ) ) ;
#15669=ORIENTED_EDGE ( 'NONE', *, *, #6163, .F. ) ;
#15682=EDGE_CURVE ( 'NONE', #11141, #13004, #12255, .T. ) ;
#15706=DIRECTION ( 'NONE',  ( -1.000000000000000000, 0.000000000000000000, 0.000000000000000000 ) ) ;
#15739=EDGE_CURVE ( 'NONE', #10014, #15650, #22428, .T. ) ;
#15769=CARTESIAN_POINT ( 'NONE',  ( -5.588000000000000078, -3694.938000000000102, 2228.849999999999909 ) ) ;
#15788=FACE_OUTER_BOUND ( 'NONE', #18131, .T. ) ;
#15803=ORIENTED_EDGE ( 'NONE', *, *, #16262, .T. ) ;
#15805=DIRECTION ( 'NONE',  ( 0.000000000000000000, 0.000000000000000000, -1.000000000000000000 ) ) ;
#15862=ORIENTED_EDGE ( 'NONE', *, *, #16934, .T. ) ;
#15868=ORIENTED_EDGE ( 'NONE', *, *, #7941, .T. ) ;
#15882=ADVANCED_FACE ( 'NONE', ( #7897 ), #14932, .T. ) ;
#15888=VERTEX_POINT ( 'NONE', #8015 ) ;
#15901=DIRECTION ( 'NONE',  ( 0.000000000000000000, 1.000000000000000000, 0.000000000000000000 ) ) ;
#15912=CARTESIAN_POINT ( 'NONE',  ( 3.810000000000000053, -3543.299999999999727, 2228.849999999999909 ) ) ;
#15948=EDGE_LOOP ( 'NONE', ( #19801, #12042, #1345, #14680 ) ) ;
#15983=AXIS2_PLACEMENT_3D ( 'NONE', #6612, #12331, #19481 ) ;
#16004=EDGE_CURVE ( 'NONE', #20079, #21067, #1561, .T. ) ;
#16016=CARTESIAN_POINT ( 'NONE',  ( 3.048000000000000043, -3694.938000000000102, 2228.849999999999909 ) ) ;
#16043=ORIENTED_EDGE ( 'NONE', *, *, #14098, .F. ) ;
#16044=CARTESIAN_POINT ( 'NONE',  ( 1.270000000000000018, -3578.860000000000127, 2250.236800000000130 ) ) ;
#16087=AXIS2_PLACEMENT_3D ( 'NONE', #6635, #17377, #1338 ) ;
#16138=DIRECTION ( 'NONE',  ( 0.000000000000000000, -1.000000000000000000, 0.000000000000000000 ) ) ;
#16149=LINE ( 'NONE', #94, #19847 ) ;
#16150=LINE ( 'NONE', #3714, #6223 ) ;
#16151=CARTESIAN_POINT ( 'NONE',  ( 3.048000000000000043, -3544.061999999999898, 2229.612000000000080 ) ) ;
#16218=DIRECTION ( 'NONE',  ( 0.000000000000000000, 0.000000000000000000, 1.000000000000000000 ) ) ;
#16230=DIRECTION ( 'NONE',  ( -1.000000000000000000, 0.000000000000000000, 0.000000000000000000 ) ) ;
#16239=CARTESIAN_POINT ( 'NONE',  ( 1.270000000000000018, -3578.860000000000127, 2247.392000000000280 ) ) ;
#16262=EDGE_CURVE ( 'NONE', #19268, #8944, #4121, .T. ) ;
#16287=CARTESIAN_POINT ( 'NONE',  ( -0.7620000000000000107, -3694.938000000000102, 2254.250000000000000 ) ) ;
#16309=DIRECTION ( 'NONE',  ( 1.000000000000000000, 0.000000000000000000, 0.000000000000000000 ) ) ;
#16331=ORIENTED_EDGE ( 'NONE', *, *, #21864, .T. ) ;
#16341=CARTESIAN_POINT ( 'NONE',  ( 0.000000000000000000, -3694.938000000000102, 2239.771999999999935 ) ) ;
#16359=VERTEX_POINT ( 'NONE', #11161 ) ;
#16382=ORIENTED_EDGE ( 'NONE', *, *, #16604, .T. ) ;
#16399=CIRCLE ( 'NONE', #997, 0.7619999999999294005 ) ;
#16416=ORIENTED_EDGE ( 'NONE', *, *, #23095, .T. ) ;
#16424=EDGE_CURVE ( 'NONE', #18606, #18259, #3081, .T. ) ;
#16445=LINE ( 'NONE', #14356, #15586 ) ;
#16453=ADVANCED_FACE ( 'NONE', ( #17423 ), #14041, .T. ) ;
#16457=EDGE_LOOP ( 'NONE', ( #6852, #842 ) ) ;
#16486=CIRCLE ( 'NONE', #10870, 0.7619999999999294005 ) ;
#16494=ORIENTED_EDGE ( 'NONE', *, *, #3219, .T. ) ;
#16516=CIRCLE ( 'NONE', #6799, 0.7619999999999294005 ) ;
#16520=ORIENTED_EDGE ( 'NONE', *, *, #1493, .T. ) ;
#16527=DIRECTION ( 'NONE',  ( 0.000000000000000000, 0.000000000000000000, 1.000000000000000000 ) ) ;
#16532=ADVANCED_FACE ( 'NONE', ( #8417 ), #6783, .T. ) ;
#16540=DIRECTION ( 'NONE',  ( 0.000000000000000000, -1.000000000000000000, 0.000000000000000000 ) ) ;
#16557=DIRECTION ( 'NONE',  ( 0.000000000000000000, 1.000000000000000000, 0.000000000000000000 ) ) ;
#16560=ORIENTED_EDGE ( 'NONE', *, *, #6163, .T. ) ;
#16579=AXIS2_PLACEMENT_3D ( 'NONE', #6516, #2746, #870 ) ;
#16604=EDGE_CURVE ( 'NONE', #19266, #18679, #20131, .T. ) ;
#16610=DIRECTION ( 'NONE',  ( 0.000000000000000000, 0.000000000000000000, 1.000000000000000000 ) ) ;
#16614=CARTESIAN_POINT ( 'NONE',  ( 0.000000000000000000, -3660.140000000000327, 2250.998800000000301 ) ) ;
#16637=CARTESIAN_POINT ( 'NONE',  ( 1.270000000000000018, -3578.860000000000127, 2247.392000000000280 ) ) ;
#16654=CARTESIAN_POINT ( 'NONE',  ( -5.588000000000000078, -3544.061999999999898, 2253.487999999999829 ) ) ;
#16659=ORIENTED_EDGE ( 'NONE', *, *, #16424, .T. ) ;
#16716=AXIS2_PLACEMENT_3D ( 'NONE', #7669, #10959, #18448 ) ;
#16741=UNCERTAINTY_MEASURE_WITH_UNIT (LENGTH_MEASURE( 1.000000000000000082E-05 ), #21126, 'distance_accuracy_value', 'NONE');
#16772=CYLINDRICAL_SURFACE ( 'NONE', #12654, 0.7619999999999294005 ) ;
#16779=DIRECTION ( 'NONE',  ( -1.000000000000000000, 0.000000000000000000, 0.000000000000000000 ) ) ;
#16793=APPLICATION_CONTEXT ( 'configuration controlled 3d designs of mechanical parts and assemblies' ) ;
#16809=AXIS2_PLACEMENT_3D ( 'NONE', #7806, #2632, #13073 ) ;
#16823=ORIENTED_EDGE ( 'NONE', *, *, #2676, .F. ) ;
#16833=DIRECTION ( 'NONE',  ( 0.000000000000000000, -1.000000000000000000, 0.000000000000000000 ) ) ;
#16835=EDGE_CURVE ( 'NONE', #22295, #4559, #7956, .T. ) ;
#16841=EDGE_CURVE ( 'NONE', #15348, #19268, #21629, .T. ) ;
#16877=CARTESIAN_POINT ( 'NONE',  ( 3.048000000000000043, -3694.938000000000102, 2238.248000000000047 ) ) ;
#16896=CIRCLE ( 'NONE', #21781, 0.7619999999999294005 ) ;
#16907=VECTOR ( 'NONE', #787, 1000.000000000000000 ) ;
#16932=ADVANCED_FACE ( 'NONE', ( #5583 ), #5710, .T. ) ;
#16934=EDGE_CURVE ( 'NONE', #8091, #2574, #21055, .T. ) ;
#16992=DIRECTION ( 'NONE',  ( 1.000000000000000000, 0.000000000000000000, 0.000000000000000000 ) ) ;
#17024=ORIENTED_EDGE ( 'NONE', *, *, #21610, .T. ) ;
#17036=CARTESIAN_POINT ( 'NONE',  ( 0.7620000000000000107, -3544.061999999999898, 2239.771999999999935 ) ) ;
#17052=DIRECTION ( 'NONE',  ( 0.000000000000000000, 1.000000000000000000, 0.000000000000000000 ) ) ;
#17055=DIRECTION ( 'NONE',  ( -1.000000000000000000, 0.000000000000000000, 0.000000000000000000 ) ) ;
#17064=EDGE_CURVE ( 'NONE', #15650, #12135, #9759, .T. ) ;
#17092=FACE_OUTER_BOUND ( 'NONE', #19027, .T. ) ;
#17107=ORIENTED_EDGE ( 'NONE', *, *, #17536, .T. ) ;
#17112=CARTESIAN_POINT ( 'NONE',  ( -0.7620000000000000107, -3660.140000000000327, 2247.392000000000280 ) ) ;
#17124=CARTESIAN_POINT ( 'NONE',  ( -0.7620000000000000107, -3694.938000000000102, 2239.771999999999935 ) ) ;
#17129=( NAMED_UNIT ( * ) SI_UNIT ( $, .STERADIAN. ) SOLID_ANGLE_UNIT ( ) );
#17136=DIRECTION ( 'NONE',  ( 0.000000000000000000, 0.000000000000000000, 1.000000000000000000 ) ) ;
#17159=CIRCLE ( 'NONE', #10426, 0.7619999999999294005 ) ;
#17178=ORIENTED_EDGE ( 'NONE', *, *, #22712, .F. ) ;
#17182=FACE_OUTER_BOUND ( 'NONE', #20411, .T. ) ;
#17229=ADVANCED_FACE ( 'NONE', ( #18529 ), #13195, .T. ) ;
#17252=DIRECTION ( 'NONE',  ( 1.000000000000000000, 0.000000000000000000, 0.000000000000000000 ) ) ;
#17272=DIRECTION ( 'NONE',  ( 0.000000000000000000, 0.000000000000000000, -1.000000000000000000 ) ) ;
#17275=ORIENTED_EDGE ( 'NONE', *, *, #21718, .T. ) ;
#17282=ORIENTED_EDGE ( 'NONE', *, *, #22253, .F. ) ;
#17308=CARTESIAN_POINT ( 'NONE',  ( -5.588000000000000078, -3544.061999999999898, 2228.849999999999909 ) ) ;
#17325=ORIENTED_EDGE ( 'NONE', *, *, #17983, .F. ) ;
#17326=ORIENTED_EDGE ( 'NONE', *, *, #7802, .T. ) ;
#17350=ORIENTED_EDGE ( 'NONE', *, *, #23162, .T. ) ;
#17377=DIRECTION ( 'NONE',  ( 1.000000000000000000, 0.000000000000000000, 0.000000000000000000 ) ) ;
#17417=AXIS2_PLACEMENT_3D ( 'NONE', #17888, #1836, #12033 ) ;
#17423=FACE_OUTER_BOUND ( 'NONE', #18008, .T. ) ;
#17439=ORIENTED_EDGE ( 'NONE', *, *, #1277, .F. ) ;
#17473=ORIENTED_EDGE ( 'NONE', *, *, #14031, .T. ) ;
#17507=DIRECTION ( 'NONE',  ( 0.000000000000000000, 0.000000000000000000, 1.000000000000000000 ) ) ;
#17516=DIRECTION ( 'NONE',  ( 0.000000000000000000, 1.000000000000000000, 0.000000000000000000 ) ) ;
#17536=EDGE_CURVE ( 'NONE', #8499, #15888, #19576, .T. ) ;
#17546=DIRECTION ( 'NONE',  ( 0.000000000000000000, 0.000000000000000000, -1.000000000000000000 ) ) ;
#17561=ORIENTED_EDGE ( 'NONE', *, *, #8524, .F. ) ;
#17563=CARTESIAN_POINT ( 'NONE',  ( 3.048000000000000043, -3695.699999999999818, 2229.612000000000080 ) ) ;
#17591=CARTESIAN_POINT ( 'NONE',  ( -0.7620000000000000107, -3578.860000000000127, 2247.392000000000280 ) ) ;
#17600=CIRCLE ( 'NONE', #11249, 0.7619999999999294005 ) ;
#17608=DIRECTION ( 'NONE',  ( 1.000000000000000000, 0.000000000000000000, 0.000000000000000000 ) ) ;
#17650=DIRECTION ( 'NONE',  ( 1.479750996568279710E-14, 0.000000000000000000, 1.000000000000000000 ) ) ;
#17664=DIRECTION ( 'NONE',  ( 1.000000000000000000, 0.000000000000000000, 0.000000000000000000 ) ) ;
#17704=ORIENTED_EDGE ( 'NONE', *, *, #12109, .T. ) ;
#17723=ORIENTED_EDGE ( 'NONE', *, *, #20102, .T. ) ;
#17764=AXIS2_PLACEMENT_3D ( 'NONE', #8834, #19148, #11884 ) ;
#17812=DIRECTION ( 'NONE',  ( 0.000000000000000000, -1.000000000000000000, 0.000000000000000000 ) ) ;
#17837=UNCERTAINTY_MEASURE_WITH_UNIT (LENGTH_MEASURE( 1.000000000000000082E-05 ), #13621, 'distance_accuracy_value', 'NONE');
#17872=DIRECTION ( 'NONE',  ( 1.000000000000000000, 0.000000000000000000, 0.000000000000000000 ) ) ;
#17888=CARTESIAN_POINT ( 'NONE',  ( -0.7620000000000000107, -3694.938000000000102, 2253.487999999999829 ) ) ;
#17921=DIRECTION ( 'NONE',  ( 0.000000000000000000, 1.000000000000000000, 0.000000000000000000 ) ) ;
#17971=EDGE_CURVE ( 'NONE', #20881, #16359, #8006, .T. ) ;
#17983=EDGE_CURVE ( 'NONE', #12671, #20881, #12290, .T. ) ;
#17986=CARTESIAN_POINT ( 'NONE',  ( -5.588000000000000078, -3660.140000000000327, 2247.392000000000280 ) ) ;
#18008=EDGE_LOOP ( 'NONE', ( #17275, #11767, #7331, #6244 ) ) ;
#18015=CIRCLE ( 'NONE', #21398, 0.7619999999999294005 ) ;
#18026=DIRECTION ( 'NONE',  ( -1.000000000000000000, 0.000000000000000000, 0.000000000000000000 ) ) ;
#18040=SPHERICAL_SURFACE ( 'NONE', #7772, 0.7620000000000000107 ) ;
#18050=ORIENTED_EDGE ( 'NONE', *, *, #1277, .T. ) ;
#18070=CARTESIAN_POINT ( 'NONE',  ( 3.048000000000000043, -3543.299999999999727, 2229.612000000000080 ) ) ;
#18094=CARTESIAN_POINT ( 'NONE',  ( -6.349999999999999645, -3544.061999999999898, 2253.487999999999829 ) ) ;
#18131=EDGE_LOOP ( 'NONE', ( #10330, #17282, #22273, #11088 ) ) ;
#18139=EDGE_LOOP ( 'NONE', ( #10965, #2555, #8723, #20755 ) ) ;
#18150=DIRECTION ( 'NONE',  ( 0.000000000000000000, 1.000000000000000000, 0.000000000000000000 ) ) ;
#18155=DIRECTION ( 'NONE',  ( 1.000000000000000000, 0.000000000000000000, 0.000000000000000000 ) ) ;
#18157=DIRECTION ( 'NONE',  ( 0.000000000000000000, 1.000000000000000000, 0.000000000000000000 ) ) ;
#18170=APPLICATION_CONTEXT ( 'configuration controlled 3d designs of mechanical parts and assemblies' ) ;
#18176=ORIENTED_EDGE ( 'NONE', *, *, #21864, .F. ) ;
#18248=EDGE_CURVE ( 'NONE', #19266, #22749, #13994, .T. ) ;
#18255=ORIENTED_EDGE ( 'NONE', *, *, #15005, .T. ) ;
#18259=VERTEX_POINT ( 'NONE', #19461 ) ;
#18263=VERTEX_POINT ( 'NONE', #1641 ) ;
#18264=DIRECTION ( 'NONE',  ( -9.070589041464213634E-14, 0.000000000000000000, -1.000000000000000000 ) ) ;
#18315=SPHERICAL_SURFACE ( 'NONE', #4177, 0.7620000000000000107 ) ;
#18432=ORIENTED_EDGE ( 'NONE', *, *, #20041, .T. ) ;
#18443=AXIS2_PLACEMENT_3D ( 'NONE', #21244, #8700, #10685 ) ;
#18448=DIRECTION ( 'NONE',  ( 0.000000000000000000, 0.000000000000000000, -1.000000000000000000 ) ) ;
#18470=AXIS2_PLACEMENT_3D ( 'NONE', #6787, #7553, #5147 ) ;
#18516=TOROIDAL_SURFACE ( 'NONE', #13708, 3.606799999999999784, 0.7620000000000000107 ) ;
#18520=CARTESIAN_POINT ( 'NONE',  ( -5.588000000000000078, -3578.860000000000127, 2250.998800000000301 ) ) ;
#18529=FACE_OUTER_BOUND ( 'NONE', #42, .T. ) ;
#18551=CYLINDRICAL_SURFACE ( 'NONE', #10351, 0.7619999999999996776 ) ;
#18553=AXIS2_PLACEMENT_3D ( 'NONE', #21313, #9120, #19786 ) ;
#18562=EDGE_CURVE ( 'NONE', #11737, #18679, #22957, .T. ) ;
#18578=DIRECTION ( 'NONE',  ( 0.000000000000000000, 0.000000000000000000, 1.000000000000000000 ) ) ;
#18582=VERTEX_POINT ( 'NONE', #1974 ) ;
#18606=VERTEX_POINT ( 'NONE', #19789 ) ;
#18662=DIRECTION ( 'NONE',  ( 0.000000000000000000, -1.000000000000000000, 0.000000000000000000 ) ) ;
#18678=ORIENTED_EDGE ( 'NONE', *, *, #10558, .T. ) ;
#18679=VERTEX_POINT ( 'NONE', #20242 ) ;
#18721=CARTESIAN_POINT ( 'NONE',  ( -5.588000000000000078, -3660.140000000000327, 2247.392000000000280 ) ) ;
#18740=EDGE_LOOP ( 'NONE', ( #17326, #6225, #14772 ) ) ;
#18767=AXIS2_PLACEMENT_3D ( 'NONE', #22179, #12940, #15046 ) ;
#18768=EDGE_LOOP ( 'NONE', ( #1816, #9187, #19790, #11922 ) ) ;
#18787=EDGE_CURVE ( 'NONE', #18259, #2462, #21993, .T. ) ;
#18805=AXIS2_PLACEMENT_3D ( 'NONE', #19717, #11031, #14785 ) ;
#18827=CYLINDRICAL_SURFACE ( 'NONE', #12195, 0.7620000000000001217 ) ;
#18832=AXIS2_PLACEMENT_3D ( 'NONE', #19232, #3165, #19701 ) ;
#18858=VERTEX_POINT ( 'NONE', #15663 ) ;
#18904=CYLINDRICAL_SURFACE ( 'NONE', #10397, 0.7620000000000000107 ) ;
#18910=VERTEX_POINT ( 'NONE', #21051 ) ;
#18924=AXIS2_PLACEMENT_3D ( 'NONE', #6705, #19463, #12079 ) ;
#18944=CARTESIAN_POINT ( 'NONE',  ( -0.7620000000000000107, -3543.299999999999727, 2253.487999999999829 ) ) ;
#18982=EDGE_CURVE ( 'NONE', #18582, #13004, #22989, .T. ) ;
#19017=DIRECTION ( 'NONE',  ( 0.000000000000000000, 1.000000000000000000, 0.000000000000000000 ) ) ;
#19020=CARTESIAN_POINT ( 'NONE',  ( -5.588000000000000078, -3578.860000000000127, 2247.392000000000280 ) ) ;
#19027=EDGE_LOOP ( 'NONE', ( #7040, #6666, #8164 ) ) ;
#19039=ORIENTED_EDGE ( 'NONE', *, *, #14395, .F. ) ;
#19053=CARTESIAN_POINT ( 'NONE',  ( -0.7620000000000000107, -3543.299999999999727, 2239.771999999999935 ) ) ;
#19057=DIRECTION ( 'NONE',  ( 1.000000000000000000, 0.000000000000000000, 0.000000000000000000 ) ) ;
#19148=DIRECTION ( 'NONE',  ( -1.000000000000000000, 0.000000000000000000, 0.000000000000000000 ) ) ;
#19159=DIRECTION ( 'NONE',  ( 0.000000000000000000, -1.000000000000000000, 0.000000000000000000 ) ) ;
#19168=CIRCLE ( 'NONE', #800, 0.7619999999999294005 ) ;
#19169=CARTESIAN_POINT ( 'NONE',  ( 0.000000000000000000, -3660.140000000000327, 2247.392000000000280 ) ) ;
#19178=AXIS2_PLACEMENT_3D ( 'NONE', #17986, #17872, #9089 ) ;
#19186=AXIS2_PLACEMENT_3D ( 'NONE', #21894, #20255, #6315 ) ;
#19187=ADVANCED_FACE ( 'NONE', ( #1295 ), #6039, .T. ) ;
#19207=ORIENTED_EDGE ( 'NONE', *, *, #21182, .F. ) ;
#19232=CARTESIAN_POINT ( 'NONE',  ( -0.7620000000000000107, -3660.140000000000327, 2247.392000000000280 ) ) ;
#19260=ORIENTED_EDGE ( 'NONE', *, *, #2969, .T. ) ;
#19263=AXIS2_PLACEMENT_3D ( 'NONE', #16239, #8978, #74 ) ;
#19266=VERTEX_POINT ( 'NONE', #11301 ) ;
#19268=VERTEX_POINT ( 'NONE', #15611 ) ;
#19276=DIRECTION ( 'NONE',  ( 1.000000000000000000, 0.000000000000000000, 0.000000000000000000 ) ) ;
#19283=ORIENTED_EDGE ( 'NONE', *, *, #14820, .F. ) ;
#19288=SPHERICAL_SURFACE ( 'NONE', #14582, 0.7620000000000000107 ) ;
#19395=DIRECTION ( 'NONE',  ( 0.000000000000000000, 1.000000000000000000, 0.000000000000000000 ) ) ;
#19445=AXIS2_PLACEMENT_3D ( 'NONE', #12709, #21503, #19747 ) ;
#19446=VERTEX_POINT ( 'NONE', #13961 ) ;
#19461=CARTESIAN_POINT ( 'NONE',  ( 3.810000000000000053, -3694.938000000000102, 2238.248000000000047 ) ) ;
#19463=DIRECTION ( 'NONE',  ( -1.000000000000000000, 0.000000000000000000, 0.000000000000000000 ) ) ;
#19481=DIRECTION ( 'NONE',  ( 0.000000000000000000, 0.000000000000000000, 1.000000000000000000 ) ) ;
#19483=AXIS2_PLACEMENT_3D ( 'NONE', #5303, #7176, #14330 ) ;
#19515=FACE_OUTER_BOUND ( 'NONE', #10730, .T. ) ;
#19542=CARTESIAN_POINT ( 'NONE',  ( 3.048000000000000043, -3694.938000000000102, 2238.248000000000047 ) ) ;
#19562=DIRECTION ( 'NONE',  ( 0.000000000000000000, -1.000000000000000000, 0.000000000000000000 ) ) ;
#19576=LINE ( 'NONE', #3513, #15096 ) ;
#19609=ADVANCED_FACE ( 'NONE', ( #2123 ), #2235, .T. ) ;
#19619=CARTESIAN_POINT ( 'NONE',  ( -6.349999999999999645, -3578.860000000000127, 2247.392000000000280 ) ) ;
#19641=ORIENTED_EDGE ( 'NONE', *, *, #10388, .T. ) ;
#19654=ORIENTED_EDGE ( 'NONE', *, *, #10388, .F. ) ;
#19701=DIRECTION ( 'NONE',  ( 0.000000000000000000, 0.000000000000000000, -1.000000000000000000 ) ) ;
#19705=CIRCLE ( 'NONE', #9593, 0.7619999999999294005 ) ;
#19717=CARTESIAN_POINT ( 'NONE',  ( -5.588000000000000078, -3694.938000000000102, 2253.487999999999829 ) ) ;
#19731=CYLINDRICAL_SURFACE ( 'NONE', #10359, 0.7620000000000001217 ) ;
#19747=DIRECTION ( 'NONE',  ( 0.000000000000000000, 0.000000000000000000, 1.000000000000000000 ) ) ;
#19758=TOROIDAL_SURFACE ( 'NONE', #20142, 1.524000000000000021, 0.7620000000000000107 ) ;
#19780=ORIENTED_EDGE ( 'NONE', *, *, #12109, .F. ) ;
#19786=DIRECTION ( 'NONE',  ( 0.000000000000000000, 0.000000000000000000, -1.000000000000000000 ) ) ;
#19789=CARTESIAN_POINT ( 'NONE',  ( 3.048000000000000043, -3695.699999999999818, 2238.248000000000047 ) ) ;
#19790=ORIENTED_EDGE ( 'NONE', *, *, #9768, .T. ) ;
#19801=ORIENTED_EDGE ( 'NONE', *, *, #7931, .T. ) ;
#19808=SPHERICAL_SURFACE ( 'NONE', #15216, 0.7620000000000000107 ) ;
#19826=ORIENTED_EDGE ( 'NONE', *, *, #10057, .F. ) ;
#19827=DIRECTION ( 'NONE',  ( 0.000000000000000000, 1.000000000000000000, 0.000000000000000000 ) ) ;
#19836=CIRCLE ( 'NONE', #16087, 0.7619999999999294005 ) ;
#19847=VECTOR ( 'NONE', #7246, 1000.000000000000000 ) ;
#19854=CYLINDRICAL_SURFACE ( 'NONE', #6324, 0.7619999999999294005 ) ;
#19856=DIRECTION ( 'NONE',  ( 0.000000000000000000, 0.000000000000000000, 1.000000000000000000 ) ) ;
#19858=LINE ( 'NONE', #16341, #14728 ) ;
#19868=DIRECTION ( 'NONE',  ( 1.000000000000000000, 0.000000000000000000, 0.000000000000000000 ) ) ;
#19902=ORIENTED_EDGE ( 'NONE', *, *, #15682, .T. ) ;
#19904=ORIENTED_EDGE ( 'NONE', *, *, #7505, .T. ) ;
#19924=AXIS2_PLACEMENT_3D ( 'NONE', #21926, #14446, #12679 ) ;
#19974=LINE ( 'NONE', #5572, #14857 ) ;
#19979=CIRCLE ( 'NONE', #5715, 0.7619999999999294005 ) ;
#20033=ORIENTED_EDGE ( 'NONE', *, *, #9378, .F. ) ;
#20041=EDGE_CURVE ( 'NONE', #22749, #11737, #11117, .T. ) ;
#20079=VERTEX_POINT ( 'NONE', #22566 ) ;
#20080=ORIENTED_EDGE ( 'NONE', *, *, #18562, .F. ) ;
#20102=EDGE_CURVE ( 'NONE', #5906, #18858, #884, .T. ) ;
#20104=ORIENTED_EDGE ( 'NONE', *, *, #3219, .F. ) ;
#20131=LINE ( 'NONE', #7580, #11308 ) ;
#20142=AXIS2_PLACEMENT_3D ( 'NONE', #11006, #18150, #21787 ) ;
#20183=VERTEX_POINT ( 'NONE', #2437 ) ;
#20185=EDGE_CURVE ( 'NONE', #4963, #5042, #14455, .T. ) ;
#20199=CIRCLE ( 'NONE', #10077, 0.7619999999999294005 ) ;
#20228=DIRECTION ( 'NONE',  ( 0.000000000000000000, 1.000000000000000000, 0.000000000000000000 ) ) ;
#20242=CARTESIAN_POINT ( 'NONE',  ( -5.588000000000000078, -3660.140000000000327, 2244.547199999999975 ) ) ;
#20245=CARTESIAN_POINT ( 'NONE',  ( 1.270000000000000018, -3660.140000000000327, 2250.236800000000130 ) ) ;
#20255=DIRECTION ( 'NONE',  ( -1.000000000000000000, 0.000000000000000000, 0.000000000000000000 ) ) ;
#20274=VECTOR ( 'NONE', #20805, 1000.000000000000000 ) ;
#20294=AXIS2_PLACEMENT_3D ( 'NONE', #12302, #1274, #20858 ) ;
#20314=EDGE_LOOP ( 'NONE', ( #5865, #16659, #8980 ) ) ;
#20338=LINE ( 'NONE', #1210, #6044 ) ;
#20340=AXIS2_PLACEMENT_3D ( 'NONE', #1218, #1454, #10129 ) ;
#20361=DIRECTION ( 'NONE',  ( 1.000000000000000000, 0.000000000000000000, 0.000000000000000000 ) ) ;
#20362=LINE ( 'NONE', #6193, #3700 ) ;
#20370=CARTESIAN_POINT ( 'NONE',  ( 3.810000000000000053, -3694.938000000000102, 2229.612000000000080 ) ) ;
#20411=EDGE_LOOP ( 'NONE', ( #22592, #9617, #17704, #9687 ) ) ;
#20424=CIRCLE ( 'NONE', #11059, 0.7619999999999996776 ) ;
#20445=ORIENTED_EDGE ( 'NONE', *, *, #4975, .F. ) ;
#20463=DIRECTION ( 'NONE',  ( -1.000000000000000000, 0.000000000000000000, 0.000000000000000000 ) ) ;
#20475=ORIENTED_EDGE ( 'NONE', *, *, #9859, .F. ) ;
#20480=ORIENTED_EDGE ( 'NONE', *, *, #21182, .T. ) ;
#20482=CIRCLE ( 'NONE', #2166, 0.7619999999999294005 ) ;
#20500=VERTEX_POINT ( 'NONE', #4615 ) ;
#20524=DIRECTION ( 'NONE',  ( 0.000000000000000000, 0.000000000000000000, -1.000000000000000000 ) ) ;
#20528=DIRECTION ( 'NONE',  ( 1.000000000000000000, 0.000000000000000000, 0.000000000000000000 ) ) ;
#20533=ADVANCED_FACE ( 'NONE', ( #6156 ), #18516, .T. ) ;
#20613=DIRECTION ( 'NONE',  ( -1.000000000000000000, 0.000000000000000000, 0.000000000000000000 ) ) ;
#20616=DIRECTION ( 'NONE',  ( 0.000000000000000000, 1.000000000000000000, -1.224646799147353207E-16 ) ) ;
#20617=CARTESIAN_POINT ( 'NONE',  ( -5.588000000000000078, -3694.938000000000102, 2253.487999999999829 ) ) ;
#20706=EDGE_CURVE ( 'NONE', #4559, #22295, #9591, .T. ) ;
#20731=PRODUCT_DEFINITION_CONTEXT ( 'detailed design', #18170, 'design' ) ;
#20755=ORIENTED_EDGE ( 'NONE', *, *, #7802, .F. ) ;
#20777=DIRECTION ( 'NONE',  ( -1.000000000000000000, 0.000000000000000000, 0.000000000000000000 ) ) ;
#20787=CIRCLE ( 'NONE', #17417, 0.7620000000000000107 ) ;
#20805=DIRECTION ( 'NONE',  ( -1.000000000000000000, 0.000000000000000000, 0.000000000000000000 ) ) ;
#20854=CARTESIAN_POINT ( 'NONE',  ( -0.7620000000000000107, -3544.061999999999898, 2253.487999999999829 ) ) ;
#20858=DIRECTION ( 'NONE',  ( 1.000000000000000000, 0.000000000000000000, 0.000000000000000000 ) ) ;
#20860=ORIENTED_EDGE ( 'NONE', *, *, #4376, .T. ) ;
#20881=VERTEX_POINT ( 'NONE', #9743 ) ;
#20888=DIRECTION ( 'NONE',  ( 1.000000000000000000, 0.000000000000000000, 0.000000000000000000 ) ) ;
#20893=SHAPE_REPRESENTATION_RELATIONSHIP ( 'NONE' , 'NONE' ,  #9499, #6029 ) ;
#20896=EDGE_CURVE ( 'NONE', #18910, #20500, #9902, .T. ) ;
#20917=CARTESIAN_POINT ( 'NONE',  ( -0.7620000000000000107, -3695.699999999999818, 2253.487999999999829 ) ) ;
#20929=ORIENTED_EDGE ( 'NONE', *, *, #1960, .T. ) ;
#20966=DIRECTION ( 'NONE',  ( -1.000000000000000000, 0.000000000000000000, 0.000000000000000000 ) ) ;
#20968=ORIENTED_EDGE ( 'NONE', *, *, #5088, .F. ) ;
#21034=DIRECTION ( 'NONE',  ( 0.000000000000000000, -1.000000000000000000, 0.000000000000000000 ) ) ;
#21051=CARTESIAN_POINT ( 'NONE',  ( -6.349999999999999645, -3544.061999999999898, 2229.612000000000080 ) ) ;
#21055=CIRCLE ( 'NONE', #7566, 3.606800000000021100 ) ;
#21063=AXIS2_PLACEMENT_3D ( 'NONE', #12996, #13210, #893 ) ;
#21067=VERTEX_POINT ( 'NONE', #2948 ) ;
#21083=MANIFOLD_SOLID_BREP ( 'SOLID259[1]', #3116 ) ;
#21126=( LENGTH_UNIT ( ) NAMED_UNIT ( * ) SI_UNIT ( .MILLI., .METRE. ) );
#21139=CARTESIAN_POINT ( 'NONE',  ( 3.048000000000000043, -3544.061999999999898, 2228.849999999999909 ) ) ;
#21143=AXIS2_PLACEMENT_3D ( 'NONE', #7088, #23120, #9190 ) ;
#21182=EDGE_CURVE ( 'NONE', #22614, #18910, #8224, .T. ) ;
#21183=CARTESIAN_POINT ( 'NONE',  ( -5.588000000000000078, -3695.699999999999818, 2253.487999999999829 ) ) ;
#21244=CARTESIAN_POINT ( 'NONE',  ( -0.7620000000000000107, -3544.061999999999898, 2253.487999999999829 ) ) ;
#21298=DIRECTION ( 'NONE',  ( 0.000000000000000000, 1.000000000000000000, 0.000000000000000000 ) ) ;
#21313=CARTESIAN_POINT ( 'NONE',  ( -0.7620000000000000107, -3578.860000000000127, 2247.392000000000280 ) ) ;
#21316=CARTESIAN_POINT ( 'NONE',  ( -5.588000000000000078, -3695.699999999999818, 2253.487999999999829 ) ) ;
#21320=PLANE ( 'NONE',  #15182 ) ;
#21341=EDGE_LOOP ( 'NONE', ( #707, #6389, #2604, #10086 ) ) ;
#21379=DIRECTION ( 'NONE',  ( 1.000000000000000000, 0.000000000000000000, 0.000000000000000000 ) ) ;
#21398=AXIS2_PLACEMENT_3D ( 'NONE', #13616, #1070, #20524 ) ;
#21413=ADVANCED_FACE ( 'NONE', ( #22689 ), #18827, .T. ) ;
#21440=VECTOR ( 'NONE', #13061, 1000.000000000000000 ) ;
#21476=VECTOR ( 'NONE', #17664, 1000.000000000000000 ) ;
#21485=EDGE_CURVE ( 'NONE', #18910, #14398, #8634, .T. ) ;
#21503=DIRECTION ( 'NONE',  ( 1.000000000000000000, 0.000000000000000000, 0.000000000000000000 ) ) ;
#21562=CARTESIAN_POINT ( 'NONE',  ( 0.7620000000000000107, -3695.699999999999818, 2239.771999999999935 ) ) ;
#21568=EDGE_CURVE ( 'NONE', #16359, #10014, #20787, .T. ) ;
#21575=CIRCLE ( 'NONE', #5860, 3.606800000000021100 ) ;
#21610=EDGE_CURVE ( 'NONE', #14398, #12135, #20424, .T. ) ;
#21617=CARTESIAN_POINT ( 'NONE',  ( 3.810000000000000053, -3544.061999999999898, 2253.487999999999829 ) ) ;
#21629=LINE ( 'NONE', #9321, #7207 ) ;
#21670=ORIENTED_EDGE ( 'NONE', *, *, #10737, .T. ) ;
#21718=EDGE_CURVE ( 'NONE', #18263, #4281, #7458, .T. ) ;
#21720=ORIENTED_EDGE ( 'NONE', *, *, #14853, .F. ) ;
#21740=ORIENTED_EDGE ( 'NONE', *, *, #4610, .T. ) ;
#21781=AXIS2_PLACEMENT_3D ( 'NONE', #15123, #20613, #11255 ) ;
#21787=DIRECTION ( 'NONE',  ( 0.000000000000000000, 0.000000000000000000, 1.000000000000000000 ) ) ;
#21844=CIRCLE ( 'NONE', #11723, 2.844800000000091700 ) ;
#21864=EDGE_CURVE ( 'NONE', #8499, #15348, #3968, .T. ) ;
#21881=DIRECTION ( 'NONE',  ( 0.000000000000000000, 0.000000000000000000, 1.000000000000000000 ) ) ;
#21891=DIRECTION ( 'NONE',  ( 0.000000000000000000, 1.000000000000000000, 0.000000000000000000 ) ) ;
#21894=CARTESIAN_POINT ( 'NONE',  ( -5.588000000000000078, -3544.061999999999898, 2229.612000000000080 ) ) ;
#21910=EDGE_CURVE ( 'NONE', #2574, #8091, #21575, .T. ) ;
#21926=CARTESIAN_POINT ( 'NONE',  ( -0.7620000000000000107, -3660.140000000000327, 2243.785200000000259 ) ) ;
#21932=LINE ( 'NONE', #5900, #9656 ) ;
#21955=CIRCLE ( 'NONE', #11852, 0.7619999999999294005 ) ;
#21983=AXIS2_PLACEMENT_3D ( 'NONE', #4458, #4350, #11596 ) ;
#21993=LINE ( 'NONE', #770, #2049 ) ;
#22021=ORIENTED_EDGE ( 'NONE', *, *, #18248, .F. ) ;
#22043=DIRECTION ( 'NONE',  ( 0.000000000000000000, 0.000000000000000000, -1.000000000000000000 ) ) ;
#22045=AXIS2_PLACEMENT_3D ( 'NONE', #22197, #11535, #9776 ) ;
#22057=DIRECTION ( 'NONE',  ( 1.000000000000000000, 0.000000000000000000, 0.000000000000000000 ) ) ;
#22086=CARTESIAN_POINT ( 'NONE',  ( -0.7620000000000000107, -3660.140000000000327, 2247.392000000000280 ) ) ;
#22095=CIRCLE ( 'NONE', #11996, 0.7619999999999294005 ) ;
#22107=ADVANCED_FACE ( 'NONE', ( #3676 ), #19854, .T. ) ;
#22130=EDGE_LOOP ( 'NONE', ( #16331, #16520, #230, #14747 ) ) ;
#22132=DIRECTION ( 'NONE',  ( 0.000000000000000000, -1.000000000000000000, 0.000000000000000000 ) ) ;
#22179=CARTESIAN_POINT ( 'NONE',  ( 3.810000000000000053, -3544.061999999999898, 2238.248000000000047 ) ) ;
#22188=DIRECTION ( 'NONE',  ( -1.000000000000000000, 0.000000000000000000, 0.000000000000000000 ) ) ;
#22195=CARTESIAN_POINT ( 'NONE',  ( 0.000000000000000000, -3578.860000000000127, 2247.392000000000280 ) ) ;
#22197=CARTESIAN_POINT ( 'NONE',  ( -6.349999999999999645, -3660.140000000000327, 2247.392000000000280 ) ) ;
#22198=DIRECTION ( 'NONE',  ( 0.000000000000000000, 0.000000000000000000, 1.000000000000000000 ) ) ;
#22220=CARTESIAN_POINT ( 'NONE',  ( -0.7620000000000000107, -3578.860000000000127, 2243.785200000000259 ) ) ;
#22253=EDGE_CURVE ( 'NONE', #2462, #18263, #20362, .T. ) ;
#22258=ORIENTED_EDGE ( 'NONE', *, *, #4855, .F. ) ;
#22261=EDGE_LOOP ( 'NONE', ( #20480, #17439, #9294, #20033 ) ) ;
#22273=ORIENTED_EDGE ( 'NONE', *, *, #18787, .F. ) ;
#22295=VERTEX_POINT ( 'NONE', #16614 ) ;
#22299=EDGE_CURVE ( 'NONE', #3849, #8091, #17159, .T. ) ;
#22394=ORIENTED_EDGE ( 'NONE', *, *, #13504, .T. ) ;
#22407=DIRECTION ( 'NONE',  ( -1.000000000000000000, 0.000000000000000000, 0.000000000000000000 ) ) ;
#22416=EDGE_LOOP ( 'NONE', ( #14598, #4629, #15329, #16043 ) ) ;
#22428=LINE ( 'NONE', #11774, #20274 ) ;
#22455=VERTEX_POINT ( 'NONE', #12150 ) ;
#22479=VECTOR ( 'NONE', #4618, 1000.000000000000000 ) ;
#22482=CARTESIAN_POINT ( 'NONE',  ( 3.048000000000000043, -3694.938000000000102, 2229.612000000000080 ) ) ;
#22528=CIRCLE ( 'NONE', #19186, 0.7619999999999294005 ) ;
#22566=CARTESIAN_POINT ( 'NONE',  ( -5.588000000000000078, -3578.860000000000127, 2244.547199999999975 ) ) ;
#22572=PLANE ( 'NONE',  #10955 ) ;
#22592=ORIENTED_EDGE ( 'NONE', *, *, #11641, .F. ) ;
#22614=VERTEX_POINT ( 'NONE', #5712 ) ;
#22627=SPHERICAL_SURFACE ( 'NONE', #13281, 0.7620000000000000107 ) ;
#22629=CARTESIAN_POINT ( 'NONE',  ( 3.810000000000000053, -3544.061999999999898, 2238.248000000000047 ) ) ;
#22659=DIRECTION ( 'NONE',  ( 0.000000000000000000, 0.000000000000000000, -1.000000000000000000 ) ) ;
#22672=PLANE ( 'NONE',  #3711 ) ;
#22688=CARTESIAN_POINT ( 'NONE',  ( -5.588000000000000078, -3544.061999999999898, 2228.849999999999909 ) ) ;
#22689=FACE_OUTER_BOUND ( 'NONE', #13107, .T. ) ;
#22692=DIRECTION ( 'NONE',  ( -1.000000000000000000, 0.000000000000000000, 0.000000000000000000 ) ) ;
#22697=EDGE_CURVE ( 'NONE', #5364, #22614, #3715, .T. ) ;
#22704=EDGE_LOOP ( 'NONE', ( #18678, #12230, #12361, #20475 ) ) ;
#22711=DIRECTION ( 'NONE',  ( 0.000000000000000000, -1.000000000000000000, 0.000000000000000000 ) ) ;
#22712=EDGE_CURVE ( 'NONE', #8944, #18606, #8964, .T. ) ;
#22718=EDGE_CURVE ( 'NONE', #22455, #7086, #4090, .T. ) ;
#22725=LINE ( 'NONE', #17563, #6601 ) ;
#22728=CARTESIAN_POINT ( 'NONE',  ( 3.048000000000000043, -3694.938000000000102, 2239.009999999999764 ) ) ;
#22731=PLANE ( 'NONE',  #8145 ) ;
#22741=DIRECTION ( 'NONE',  ( 0.000000000000000000, 0.000000000000000000, 1.000000000000000000 ) ) ;
#22743=EDGE_CURVE ( 'NONE', #767, #18606, #8031, .T. ) ;
#22749=VERTEX_POINT ( 'NONE', #11311 ) ;
#22851=CARTESIAN_POINT ( 'NONE',  ( -6.349999999999999645, -3694.938000000000102, 2229.612000000000080 ) ) ;
#22875=EDGE_CURVE ( 'NONE', #20881, #14896, #6394, .T. ) ;
#22907=AXIS2_PLACEMENT_3D ( 'NONE', #4125, #9738, #22043 ) ;
#22911=LINE ( 'NONE', #16016, #9878 ) ;
#22912=CIRCLE ( 'NONE', #5734, 0.7620000000000001217 ) ;
#22917=DIRECTION ( 'NONE',  ( 0.000000000000000000, 0.000000000000000000, 1.000000000000000000 ) ) ;
#22940=ADVANCED_FACE ( 'NONE', ( #15646 ), #8151, .T. ) ;
#22948=AXIS2_PLACEMENT_3D ( 'NONE', #20854, #10179, #8435 ) ;
#22957=CIRCLE ( 'NONE', #5399, 2.844800000000091700 ) ;
#22989=CIRCLE ( 'NONE', #12902, 0.7619999999999294005 ) ;
#22991=VECTOR ( 'NONE', #22188, 1000.000000000000000 ) ;
#22995=ORIENTED_EDGE ( 'NONE', *, *, #14477, .F. ) ;
#23019=CARTESIAN_POINT ( 'NONE',  ( -5.588000000000000078, -3544.061999999999898, 2253.487999999999829 ) ) ;
#23021=EDGE_CURVE ( 'NONE', #7518, #19268, #19836, .T. ) ;
#23041=ORIENTED_EDGE ( 'NONE', *, *, #6427, .F. ) ;
#23070=DIRECTION ( 'NONE',  ( 1.000000000000000000, 0.000000000000000000, 0.000000000000000000 ) ) ;
#23087=CARTESIAN_POINT ( 'NONE',  ( -5.588000000000000078, -3544.061999999999898, 2229.612000000000080 ) ) ;
#23094=( NAMED_UNIT ( * ) SI_UNIT ( $, .STERADIAN. ) SOLID_ANGLE_UNIT ( ) );
#23095=EDGE_CURVE ( 'NONE', #18679, #11737, #11963, .T. ) ;
#23096=DIRECTION ( 'NONE',  ( 0.000000000000000000, 0.000000000000000000, 1.000000000000000000 ) ) ;
#23120=DIRECTION ( 'NONE',  ( 0.000000000000000000, 1.000000000000000000, 0.000000000000000000 ) ) ;
#23121=DIRECTION ( 'NONE',  ( 0.000000000000000000, 0.000000000000000000, -1.000000000000000000 ) ) ;
#23126=CARTESIAN_POINT ( 'NONE',  ( 3.048000000000000043, -3694.938000000000102, 2239.009999999999764 ) ) ;
#23162=EDGE_CURVE ( 'NONE', #12135, #9973, #14700, .T. ) ;
#23187=COLOUR_RGB('Light Blue',0.38,0.62,0.78);
#23188=FILL_AREA_STYLE_COLOUR('',#23187);
#23189=FILL_AREA_STYLE('',(#23188));
#23190=SURFACE_STYLE_FILL_AREA(#23189);
#23191=SURFACE_SIDE_STYLE('',(#23190));
#23192=SURFACE_STYLE_USAGE(.BOTH.,#23191);
#23193=PRESENTATION_STYLE_ASSIGNMENT((#23192));
#23235=STYLED_ITEM('',(#23193),#21083);
#23237=MECHANICAL_DESIGN_GEOMETRIC_PRESENTATION_REPRESENTATION('',(#23235),#2257);
ENDSEC;
END-ISO-10303-21;
